ISO-10303-21;
HEADER;
FILE_DESCRIPTION (('STEP AP214'),
    '1' );
FILE_NAME ('hex flange nut gradea_iso_ISO - 4161 - M5 - N.step',
    '2026-10-24T11:01:53',
    ( '' ),
    ( '' ),
    'SwSTEP 2.0',
    'SolidWorks 2026',
    '' );
FILE_SCHEMA (( 'AUTOMOTIVE_DESIGN' ));
ENDSEC;

DATA;
#3=CARTESIAN_POINT ( 'NONE',  ( 0.000000000000000000, 0.000000000000000000, -4.694516984716113228 ) ) ;
#5=ORIENTED_EDGE ( 'NONE', *, *, #5962, .F. ) ;
#7=EDGE_CURVE ( 'NONE', #1026, #1114, #8022, .T. ) ;
#9=APPLICATION_CONTEXT ( 'automotive_design' ) ;
#15=DIRECTION ( 'NONE',  ( 1.000000000000000000, 0.000000000000000000, 0.000000000000000000 ) ) ;
#22=ORIENTED_EDGE ( 'NONE', *, *, #3719, .T. ) ;
#33=STYLED_ITEM('',(#8671),#7573);
#38=MECHANICAL_DESIGN_GEOMETRIC_PRESENTATION_REPRESENTATION('',(#7560),#3810);
#41=ORIENTED_EDGE ( 'NONE', *, *, #7818, .F. ) ;
#53=UNCERTAINTY_MEASURE_WITH_UNIT (LENGTH_MEASURE( 1.000000000000000082E-05 ), #4971, 'distance_accuracy_value', 'NONE');
#91=CARTESIAN_POINT ( 'NONE',  ( 0.000000000000000000, 0.000000000000000000, -0.2800830152838844622 ) ) ;
#96=ORIENTED_EDGE ( 'NONE', *, *, #1118, .T. ) ;
#102=CARTESIAN_POINT ( 'NONE',  ( 0.3461262719736147297, -4.658553426539303821, -3.671615880910379381 ) ) ;
#105=B_SPLINE_CURVE_WITH_KNOTS ( 'NONE', 3,
 ( #4717, #2155, #226, #4890, #3459, #8039 ),
 .UNSPECIFIED., .F., .F.,
 ( 4, 2, 4 ),
 ( 0.003358874760055551890, 0.004541967308452098118, 0.005725059856848645212 ),
 .UNSPECIFIED. ) ;
#107=CARTESIAN_POINT ( 'NONE',  ( -4.154094228333736538, -2.398367420967545627, -3.721909803043222276 ) ) ;
#110=CARTESIAN_POINT ( 'NONE',  ( 0.3208286057739604957, -4.433571671609698228, -0.3503314178412692548 ) ) ;
#118=CARTESIAN_POINT ( 'NONE',  ( -2.855764796983342624, 2.970025579236414082, -0.09382832055445475272 ) ) ;
#122=CARTESIAN_POINT ( 'NONE',  ( 0.000000000000000000, 0.000000000000000000, -4.974599999999998801 ) ) ;
#131=DIRECTION ( 'NONE',  ( 0.5000000000000013323, -0.8660254037844379305, 0.000000000000000000 ) ) ;
#137=( NAMED_UNIT ( * ) PLANE_ANGLE_UNIT ( ) SI_UNIT ( $, .RADIAN. ) );
#154=CARTESIAN_POINT ( 'NONE',  ( 0.5469614295415388128, -4.303013824935362663, -3.535263753543555598 ) ) ;
#165=AXIS2_PLACEMENT_3D ( 'NONE', #4222, #789, #916 ) ;
#168=LINE ( 'NONE', #4141, #8472 ) ;
#172=EDGE_CURVE ( 'NONE', #3127, #1490, #6613, .T. ) ;
#175=EDGE_CURVE ( 'NONE', #7885, #4775, #2327, .T. ) ;
#181=CARTESIAN_POINT ( 'NONE',  ( -0.5449313310646672903, -4.304185902836978883, -3.316620875263469159 ) ) ;
#192=EDGE_LOOP ( 'NONE', ( #1418, #8130, #7597, #2442 ) ) ;
#194=DIRECTION ( 'NONE',  ( -1.000000000000000000, 0.000000000000000000, 0.000000000000000000 ) ) ;
#210=DIRECTION ( 'NONE',  ( 0.5000000000000022204, 0.8660254037844374864, -0.000000000000000000 ) ) ;
#217=CARTESIAN_POINT ( 'NONE',  ( -1.393927851585477606, 4.043713361053528743, -3.526374918436835149 ) ) ;
#218=PRESENTATION_STYLE_ASSIGNMENT (( #6840 ) ) ;
#225=CARTESIAN_POINT ( 'NONE',  ( -4.175002511812151873, -2.208363329454905877, -3.469254087858246738 ) ) ;
#226=CARTESIAN_POINT ( 'NONE',  ( 4.000000000000000000, -1.560351142792952617, -0.2242961665059816367 ) ) ;
#248=ORIENTED_EDGE ( 'NONE', *, *, #3329, .F. ) ;
#262=FILL_AREA_STYLE_COLOUR ( '', #7978 ) ;
#264=CARTESIAN_POINT ( 'NONE',  ( -6.259644161404860030E-16, -4.618802153517027165, -5.000000000000000000 ) ) ;
#275=AXIS2_PLACEMENT_3D ( 'NONE', #2564, #1326, #1164 ) ;
#280=EDGE_LOOP ( 'NONE', ( #1138, #316, #2891, #6208 ) ) ;
#285=B_SPLINE_CURVE_WITH_KNOTS ( 'NONE', 3,
 ( #8294, #4931, #1495, #2332, #6091, #6272 ),
 .UNSPECIFIED., .F., .F.,
 ( 4, 2, 4 ),
 ( 0.002365888236228001588, 0.003551327329835089319, 0.004736766423442177049 ),
 .UNSPECIFIED. ) ;
#291=CARTESIAN_POINT ( 'NONE',  ( 4.211140560182196957, 2.431303136016536470, -3.745885042887433514 ) ) ;
#302=B_SPLINE_CURVE_WITH_KNOTS ( 'NONE', 3,
 ( #1517, #107, #2781, #5426, #8101, #4823 ),
 .UNSPECIFIED., .F., .F.,
 ( 4, 2, 4 ),
 ( -3.640115492409406142E-06, 0.0002066546034006526487, 0.0004169493222937146744 ),
 .UNSPECIFIED. ) ;
#305=ORIENTED_EDGE ( 'NONE', *, *, #3009, .T. ) ;
#307=DIRECTION ( 'NONE',  ( -1.000000000000000000, 0.000000000000000000, 0.000000000000000000 ) ) ;
#311=DIRECTION ( 'NONE',  ( 1.000000000000000000, 0.000000000000000000, 0.000000000000000000 ) ) ;
#312=AXIS2_PLACEMENT_3D ( 'NONE', #2273, #7297, #3257 ) ;
#315=CARTESIAN_POINT ( 'NONE',  ( 0.02511973781850649831, -4.877415612947427981, -3.751298745799844792 ) ) ;
#316=ORIENTED_EDGE ( 'NONE', *, *, #4226, .F. ) ;
#328=ORIENTED_EDGE ( 'NONE', *, *, #4280, .F. ) ;
#350=ORIENTED_EDGE ( 'NONE', *, *, #4139, .T. ) ;
#360=ORIENTED_EDGE ( 'NONE', *, *, #4499, .F. ) ;
#364=CARTESIAN_POINT ( 'NONE',  ( 2.000000000000005329, -3.464101615137751722, 0.000000000000000000 ) ) ;
#368=CONICAL_SURFACE ( 'NONE', #4533, 2.500000000000000888, 0.9599310885968785900 ) ;
#384=DIRECTION ( 'NONE',  ( 0.000000000000000000, 0.000000000000000000, -1.000000000000000000 ) ) ;
#392=VERTEX_POINT ( 'NONE', #5029 ) ;
#396=CARTESIAN_POINT ( 'NONE',  ( -0.02511973781850462134, 4.877415612947412882, -3.751298745799839462 ) ) ;
#398=B_SPLINE_CURVE_WITH_KNOTS ( 'NONE', 3,
 ( #1284, #3902, #6544, #5158, #1908 ),
 .UNSPECIFIED., .F., .F.,
 ( 4, 1, 4 ),
 ( 0.000000000000000000, 0.002309401076758505356, 0.004618802153517010713 ),
 .UNSPECIFIED. ) ;
#400=EDGE_CURVE ( 'NONE', #4773, #8282, #7861, .T. ) ;
#409=CARTESIAN_POINT ( 'NONE',  ( -3.264650091097280831E-13, -4.796980096169642493, -3.721999068284424617 ) ) ;
#423=CARTESIAN_POINT ( 'NONE',  ( 4.207491450040567571, -2.029819825146485179, -3.671670828759567407 ) ) ;
#432=B_SPLINE_CURVE_WITH_KNOTS ( 'NONE', 3,
 ( #1179, #5739, #3008, #8415, #2453 ),
 .UNSPECIFIED., .F., .F.,
 ( 4, 1, 4 ),
 ( 5.640274452250024914E-20, 0.002309401076758505356, 0.004618802153517010713 ),
 .UNSPECIFIED. ) ;
#441=CONICAL_SURFACE ( 'NONE', #1976, 4.000000000000000000, 0.8911886515913786111 ) ;
#442=EDGE_CURVE ( 'NONE', #5816, #1280, #2302, .T. ) ;
#464=DIRECTION ( 'NONE',  ( 0.000000000000000000, 0.000000000000000000, 1.000000000000000000 ) ) ;
#465=CARTESIAN_POINT ( 'NONE',  ( -4.000000000000000000, 2.309401076758498483, -0.4999999999999927280 ) ) ;
#486=FACE_OUTER_BOUND ( 'NONE', #2041, .T. ) ;
#493=DIRECTION ( 'NONE',  ( -0.000000000000000000, -0.000000000000000000, 1.000000000000000000 ) ) ;
#502=CYLINDRICAL_SURFACE ( 'NONE', #5643, 2.500000000000000444 ) ;
#508=EDGE_CURVE ( 'NONE', #7885, #3408, #1188, .T. ) ;
#535=CONICAL_SURFACE ( 'NONE', #1230, 5.560781378645573980, 1.221730476396046816 ) ;
#536=DIRECTION ( 'NONE',  ( 0.000000000000000000, 0.000000000000000000, -1.000000000000000000 ) ) ;
#550=CONICAL_SURFACE ( 'NONE', #6527, 2.059999999999998721, 0.9599310885968738161 ) ;
#562=FACE_OUTER_BOUND ( 'NONE', #280, .T. ) ;
#566=LINE ( 'NONE', #5394, #3941 ) ;
#579=CARTESIAN_POINT ( 'NONE',  ( 4.000000000000000000, 0.3987449864460005378, -0.01220643443059817035 ) ) ;
#584=( BOUNDED_SURFACE ( )  B_SPLINE_SURFACE ( 3, 2, ( 
 ( #4413, #7770, #1723 ),
 ( #3024, #1021, #1677 ),
 ( #7641, #1106, #4324 ),
 ( #3677, #4282, #6930 ),
 ( #7022, #6323, #5671 ),
 ( #8340, #2381, #3759 ) ),
 .UNSPECIFIED., .F., .F., .T. ) 
 B_SPLINE_SURFACE_WITH_KNOTS ( ( 4, 2, 4 ),
 ( 3, 3 ),
 ( 0.02027752710269158445, 0.02273781595091097299, 0.02519810479913036153 ),
 ( 0.000000000000000000, 1.000000000000000000 ),
 .UNSPECIFIED. ) 
 GEOMETRIC_REPRESENTATION_ITEM ( )  RATIONAL_B_SPLINE_SURFACE ( (
 ( 1.000000000000000000, 0.8047781431712808242, 1.000000000000000000),
 ( 1.000000000000000000, 0.8123773247083928561, 1.000000000000000000),
 ( 1.000000000000000000, 0.8190670192154906326, 1.000000000000000000),
 ( 1.000000000000000000, 0.8192353552912178261, 1.000000000000000000),
 ( 1.000000000000000000, 0.8126132098226825917, 1.000000000000000000),
 ( 1.000000000000000000, 0.8047712465856394770, 1.000000000000000000) ) ) 
 REPRESENTATION_ITEM ( '' )  SURFACE ( )  );
#594=AXIS2_PLACEMENT_3D ( 'NONE', #3123, #464, #5764 ) ;
#596=VERTEX_POINT ( 'NONE', #3235 ) ;
#623=CARTESIAN_POINT ( 'NONE',  ( 4.154306624731035846, -2.398490048085128556, -3.721999068284417955 ) ) ;
#639=CARTESIAN_POINT ( 'NONE',  ( -6.259644161404860030E-16, -4.618802153517027165, -3.433295621305388234 ) ) ;
#648=DIRECTION ( 'NONE',  ( -1.000000000000000000, 0.000000000000000000, 0.000000000000000000 ) ) ;
#652=CARTESIAN_POINT ( 'NONE',  ( 0.6507732100473444525, -4.243078065514795050, -0.2236248678334952777 ) ) ;
#653=CIRCLE ( 'NONE', #5515, 5.560781378645573980 ) ;
#658=EDGE_LOOP ( 'NONE', ( #8272, #6605, #4968, #328 ) ) ;
#670=CARTESIAN_POINT ( 'NONE',  ( -2.000000000000006661, 3.464101615137750834, 0.000000000000000000 ) ) ;
#682=VECTOR ( 'NONE', #1278, 1000.000000000000000 ) ;
#688=CARTESIAN_POINT ( 'NONE',  ( -1.828356344711647319, -3.563200125723192002, -1.076197711133951296E-14 ) ) ;
#703=CARTESIAN_POINT ( 'NONE',  ( -4.154094228333456762, 2.398367420968013253, -3.721909803043220055 ) ) ;
#709=DIRECTION ( 'NONE',  ( -0.000000000000000000, -0.000000000000000000, 1.000000000000000000 ) ) ;
#717=CARTESIAN_POINT ( 'NONE',  ( 0.000000000000000000, 0.000000000000000000, -5.000000000000000000 ) ) ;
#718=CARTESIAN_POINT ( 'NONE',  ( 0.6448876103708359731, 4.246476118072354922, -0.2256878752776725616 ) ) ;
#735=AXIS2_PLACEMENT_3D ( 'NONE', #5336, #5207, #3342 ) ;
#737=FACE_OUTER_BOUND ( 'NONE', #3619, .T. ) ;
#746=ORIENTED_EDGE ( 'NONE', *, *, #4372, .F. ) ;
#748=ADVANCED_FACE ( 'NONE', ( #7933 ), #368, .F. ) ;
#750=( GEOMETRIC_REPRESENTATION_CONTEXT ( 3 ) GLOBAL_UNCERTAINTY_ASSIGNED_CONTEXT ( ( #53 ) ) GLOBAL_UNIT_ASSIGNED_CONTEXT ( ( #4971, #4232, #7588 ) ) REPRESENTATION_CONTEXT ( 'NONE', 'WORKASPACE' ) );
#759=ADVANCED_BREP_SHAPE_REPRESENTATION ( '', ( #7573, #594 ), #750 ) ;
#764=FACE_OUTER_BOUND ( 'NONE', #6922, .T. ) ;
#771=VERTEX_POINT ( 'NONE', #3578 ) ;
#774=CARTESIAN_POINT ( 'NONE',  ( 4.211140560182196957, -2.431303136016555122, -3.745885042887436622 ) ) ;
#778=ORIENTED_EDGE ( 'NONE', *, *, #8445, .T. ) ;
#782=CARTESIAN_POINT ( 'NONE',  ( 1.411581201560190495E-15, 4.862606272033091592, -3.745885042887436622 ) ) ;
#784=CARTESIAN_POINT ( 'NONE',  ( 2.000000000000005329, -3.464101615137751722, 0.000000000000000000 ) ) ;
#789=DIRECTION ( 'NONE',  ( 0.000000000000000000, 0.000000000000000000, -1.000000000000000000 ) ) ;
#803=FACE_OUTER_BOUND ( 'NONE', #6038, .T. ) ;
#805=DIRECTION ( 'NONE',  ( 0.000000000000000000, 0.000000000000000000, -1.000000000000000000 ) ) ;
#812=DIRECTION ( 'NONE',  ( -1.000000000000000000, 0.000000000000000000, 0.000000000000000000 ) ) ;
#813=ORIENTED_EDGE ( 'NONE', *, *, #6403, .F. ) ;
#831=FACE_OUTER_BOUND ( 'NONE', #6393, .T. ) ;
#866=CARTESIAN_POINT ( 'NONE',  ( 2.548804901056335857E-15, 4.736522675502163437, -3.681124513963624612 ) ) ;
#869=CARTESIAN_POINT ( 'NONE',  ( 3.861362476283255685, 2.629030857715988656, -3.671615880910370500 ) ) ;
#876=AXIS2_PLACEMENT_3D ( 'NONE', #2223, #1481, #4744 ) ;
#880=EDGE_CURVE ( 'NONE', #8131, #2382, #653, .T. ) ;
#881=CONICAL_SURFACE ( 'NONE', #165, 4.000000000000000000, 0.8911886515913786111 ) ;
#883=LINE ( 'NONE', #8289, #1936 ) ;
#885=CARTESIAN_POINT ( 'NONE',  ( -1.747541505913277282, 3.837784562140256650, -3.503702292528906526 ) ) ;
#901=ORIENTED_EDGE ( 'NONE', *, *, #7008, .T. ) ;
#913=CARTESIAN_POINT ( 'NONE',  ( 4.175648173966055587, -2.207990556236547608, -3.469390959564065291 ) ) ;
#914=EDGE_CURVE ( 'NONE', #6725, #5979, #5528, .T. ) ;
#916=DIRECTION ( 'NONE',  ( -1.000000000000000000, 0.000000000000000000, 0.000000000000000000 ) ) ;
#917=VERTEX_POINT ( 'NONE', #3142 ) ;
#926=VERTEX_POINT ( 'NONE', #5784 ) ;
#927=DIRECTION ( 'NONE',  ( -0.000000000000000000, 0.000000000000000000, -1.000000000000000000 ) ) ;
#941=ORIENTED_EDGE ( 'NONE', *, *, #8359, .F. ) ;
#947=ORIENTED_EDGE ( 'NONE', *, *, #3635, .F. ) ;
#956=CARTESIAN_POINT ( 'NONE',  ( -2.804994570502171047, -3.229033611042465335, -3.526374918436838701 ) ) ;
#964=DIRECTION ( 'NONE',  ( -0.8660254037844373753, 0.5000000000000021094, 0.000000000000000000 ) ) ;
#982=ORIENTED_EDGE ( 'NONE', *, *, #4280, .T. ) ;
#985=DIRECTION ( 'NONE',  ( -0.000000000000000000, 0.000000000000000000, -1.000000000000000000 ) ) ;
#987=ORIENTED_EDGE ( 'NONE', *, *, #3596, .T. ) ;
#988=CARTESIAN_POINT ( 'NONE',  ( 0.000000000000000000, 0.000000000000000000, -25.03750572909317285 ) ) ;
#1012=TOROIDAL_SURFACE ( 'NONE', #7821, 5.384454397937118664, 0.5155456020628804703 ) ;
#1017=ADVANCED_FACE ( 'NONE', ( #7760 ), #5634, .T. ) ;
#1021=CARTESIAN_POINT ( 'NONE',  ( -4.000000000000000000, 1.677772373332757194, -3.535253723897187506 ) ) ;
#1026=VERTEX_POINT ( 'NONE', #7719 ) ;
#1027=ORIENTED_EDGE ( 'NONE', *, *, #1401, .F. ) ;
#1037=ORIENTED_EDGE ( 'NONE', *, *, #3856, .T. ) ;
#1039=CARTESIAN_POINT ( 'NONE',  ( -4.197393957002303999, -7.773935952363655451E-14, -3.503767560748929810 ) ) ;
#1044=VERTEX_POINT ( 'NONE', #3097 ) ;
#1057=CARTESIAN_POINT ( 'NONE',  ( 4.211140560182196957, 2.431303136016536470, -3.745885042887433514 ) ) ;
#1073=FACE_OUTER_BOUND ( 'NONE', #5412, .T. ) ;
#1074=ORIENTED_EDGE ( 'NONE', *, *, #175, .T. ) ;
#1082=CARTESIAN_POINT ( 'NONE',  ( 4.198928548860774157, -0.8158838809860124996, -3.526471437616918170 ) ) ;
#1098=ORIENTED_EDGE ( 'NONE', *, *, #8359, .T. ) ;
#1101=CARTESIAN_POINT ( 'NONE',  ( 1.390230914382191596, 4.043987460488659202, -3.502507215260488582 ) ) ;
#1106=CARTESIAN_POINT ( 'NONE',  ( -4.000000000000000000, 0.8576368993457507139, -3.433240632782198709 ) ) ;
#1114=VERTEX_POINT ( 'NONE', #784 ) ;
#1116=ADVANCED_FACE ( 'NONE', ( #1925 ), #7880, .F. ) ;
#1118=EDGE_CURVE ( 'NONE', #1114, #771, #5655, .T. ) ;
#1119=DIRECTION ( 'NONE',  ( 0.000000000000000000, 0.000000000000000000, 1.000000000000000000 ) ) ;
#1122=ADVANCED_FACE ( 'NONE', ( #737 ), #4478, .F. ) ;
#1138=ORIENTED_EDGE ( 'NONE', *, *, #4139, .F. ) ;
#1164=DIRECTION ( 'NONE',  ( -1.000000000000000000, 0.000000000000000000, 0.000000000000000000 ) ) ;
#1179=CARTESIAN_POINT ( 'NONE',  ( -6.259644161404860030E-16, -4.618802153517027165, -3.433295621305388234 ) ) ;
#1187=CARTESIAN_POINT ( 'NONE',  ( 3.472371940585993855, 2.614027278893175321, -3.320322319201766792 ) ) ;
#1188=B_SPLINE_CURVE_WITH_KNOTS ( 'NONE', 3,
 ( #3899, #6542, #5890, #5144, #1804, #8424 ),
 .UNSPECIFIED., .F., .F.,
 ( 4, 2, 4 ),
 ( 0.002365888236227977302, 0.003551327329835078910, 0.004736766423442180518 ),
 .UNSPECIFIED. ) ;
#1211=ORIENTED_EDGE ( 'NONE', *, *, #3119, .F. ) ;
#1222=ORIENTED_EDGE ( 'NONE', *, *, #2485, .T. ) ;
#1230=AXIS2_PLACEMENT_3D ( 'NONE', #2656, #5257, #6524 ) ;
#1235=CARTESIAN_POINT ( 'NONE',  ( -2.499999999999999556, 3.061616997868382648E-16, 3.469446951953614189E-15 ) ) ;
#1247=LINE ( 'NONE', #3956, #2037 ) ;
#1252=ORIENTED_EDGE ( 'NONE', *, *, #5282, .T. ) ;
#1256=CARTESIAN_POINT ( 'NONE',  ( 4.000000000000000000, -0.8732470631449981147, -3.223155494240760088 ) ) ;
#1258=VERTEX_POINT ( 'NONE', #3524 ) ;
#1261=EDGE_CURVE ( 'NONE', #5979, #7074, #6906, .T. ) ;
#1270=PRODUCT ( 'hex flange nut gradea_iso_ISO - 4161 - M5 - N', 'hex flange nut gradea_iso_ISO - 4161 - M5 - N', '', ( #4162 ) ) ;
#1278=DIRECTION ( 'NONE',  ( 0.000000000000000000, 0.000000000000000000, 1.000000000000000000 ) ) ;
#1280=VERTEX_POINT ( 'NONE', #8187 ) ;
#1284=CARTESIAN_POINT ( 'NONE',  ( 4.000000000000000000, 2.309401076758497151, -3.433295621305379353 ) ) ;
#1298=DIRECTION ( 'NONE',  ( 0.000000000000000000, 0.000000000000000000, -1.000000000000000000 ) ) ;
#1299=DIRECTION ( 'NONE',  ( 0.000000000000000000, 0.000000000000000000, 1.000000000000000000 ) ) ;
#1300=EDGE_CURVE ( 'NONE', #7097, #1468, #7100, .T. ) ;
#1315=EDGE_CURVE ( 'NONE', #7355, #5816, #3886, .T. ) ;
#1319=CARTESIAN_POINT ( 'NONE',  ( 0.000000000000000000, 0.000000000000000000, -0.3080913168122742518 ) ) ;
#1326=DIRECTION ( 'NONE',  ( -0.000000000000000000, 0.000000000000000000, -1.000000000000000000 ) ) ;
#1343=DIRECTION ( 'NONE',  ( 0.000000000000000000, 0.000000000000000000, 1.000000000000000000 ) ) ;
#1347=ORIENTED_EDGE ( 'NONE', *, *, #6080, .F. ) ;
#1350=CARTESIAN_POINT ( 'NONE',  ( 0.1750025118121568690, 4.719839900820621104, -3.469254087858248070 ) ) ;
#1351=EDGE_CURVE ( 'NONE', #392, #596, #1921, .T. ) ;
#1361=LINE ( 'NONE', #4625, #8352 ) ;
#1365=ORIENTED_EDGE ( 'NONE', *, *, #1460, .T. ) ;
#1372=CARTESIAN_POINT ( 'NONE',  ( 1.734723475976807094E-15, 4.618802153517012954, -0.4999999999999995559 ) ) ;
#1379=DIRECTION ( 'NONE',  ( 0.000000000000000000, 0.000000000000000000, -1.000000000000000000 ) ) ;
#1396=CARTESIAN_POINT ( 'NONE',  ( 0.02448733951239481094, 4.877042772274728044, -3.751161874094022242 ) ) ;
#1401=EDGE_CURVE ( 'NONE', #3609, #917, #3778, .T. ) ;
#1418=ORIENTED_EDGE ( 'NONE', *, *, #8394, .F. ) ;
#1432=CIRCLE ( 'NONE', #3936, 4.000000000000000000 ) ;
#1433=AXIS2_PLACEMENT_3D ( 'NONE', #6787, #210, #964 ) ;
#1434=CARTESIAN_POINT ( 'NONE',  ( 1.317756351988342622, -3.857995168970215438, -0.04852650426602527628 ) ) ;
#1435=CARTESIAN_POINT ( 'NONE',  ( 3.510273485745307731, 2.827716139362654424, -3.610536846335885564 ) ) ;
#1443=B_SPLINE_CURVE_WITH_KNOTS ( 'NONE', 3,
 ( #8284, #4878, #4791, #118, #7400, #2790, #4101, #2142 ),
 .UNSPECIFIED., .F., .F.,
 ( 4, 2, 2, 4 ),
 ( 2.465131517071352357E-07, 0.001183067374689843057, 0.001774477805458910071, 0.002365888236227977302 ),
 .UNSPECIFIED. ) ;
#1452=DIRECTION ( 'NONE',  ( 0.9396926207859138680, 1.150791560227856926E-16, -0.3420201433256536139 ) ) ;
#1453=ORIENTED_EDGE ( 'NONE', *, *, #7637, .F. ) ;
#1455=ORIENTED_EDGE ( 'NONE', *, *, #6019, .F. ) ;
#1460=EDGE_CURVE ( 'NONE', #917, #5858, #1247, .T. ) ;
#1468=VERTEX_POINT ( 'NONE', #4896 ) ;
#1474=CARTESIAN_POINT ( 'NONE',  ( -0.1404048886732797152, -4.699864953788083888, -3.686887068327043160 ) ) ;
#1481=DIRECTION ( 'NONE',  ( -0.000000000000000000, -0.000000000000000000, 1.000000000000000000 ) ) ;
#1483=ORIENTED_EDGE ( 'NONE', *, *, #508, .F. ) ;
#1490=VERTEX_POINT ( 'NONE', #5285 ) ;
#1495=CARTESIAN_POINT ( 'NONE',  ( -2.682243648011671588, -3.070208061305317759, -0.04852650426602272971 ) ) ;
#1508=CARTESIAN_POINT ( 'NONE',  ( -5.384454397937118664, 6.594054843588581554E-16, -4.484454397937119197 ) ) ;
#1514=VERTEX_POINT ( 'NONE', #639 ) ;
#1515=EDGE_CURVE ( 'NONE', #7956, #6857, #4954, .T. ) ;
#1516=ORIENTED_EDGE ( 'NONE', *, *, #6611, .T. ) ;
#1517=CARTESIAN_POINT ( 'NONE',  ( -4.211140560182196957, -2.431303136016552013, -3.745885042887436178 ) ) ;
#1522=ORIENTED_EDGE ( 'NONE', *, *, #1652, .T. ) ;
#1546=CARTESIAN_POINT ( 'NONE',  ( 0.000000000000000000, 0.000000000000000000, 0.000000000000000000 ) ) ;
#1561=FACE_OUTER_BOUND ( 'NONE', #6059, .T. ) ;
#1564=CARTESIAN_POINT ( 'NONE',  ( 3.522875095019493141, -2.820352903225631369, -3.598441714920572299 ) ) ;
#1568=ORIENTED_EDGE ( 'NONE', *, *, #5736, .F. ) ;
#1569=CONICAL_SURFACE ( 'NONE', #876, 2.059999999999998721, 0.9599310885968738161 ) ;
#1583=AXIS2_PLACEMENT_3D ( 'NONE', #4984, #985, #1814 ) ;
#1584=CARTESIAN_POINT ( 'NONE',  ( 0.000000000000000000, 0.000000000000000000, -4.484454397937119197 ) ) ;
#1586=CARTESIAN_POINT ( 'NONE',  ( 3.679171394226031122, 2.494631558665830973, -0.3503314178412474389 ) ) ;
#1595=CONICAL_SURFACE ( 'NONE', #6455, 4.000000000000000000, 0.8911886515913786111 ) ;
#1608=CARTESIAN_POINT ( 'NONE',  ( 2.804994570502171047, 3.229033611042449792, -3.526374918436834704 ) ) ;
#1613=CARTESIAN_POINT ( 'NONE',  ( -4.175648173966055587, 2.207990556236529844, -3.469390959564062626 ) ) ;
#1623=ADVANCED_FACE ( 'NONE', ( #2205 ), #3011, .F. ) ;
#1624=SHAPE_REPRESENTATION_RELATIONSHIP ( 'NONE' , 'NONE' ,  #4754, #759 ) ;
#1648=ORIENTED_EDGE ( 'NONE', *, *, #1351, .T. ) ;
#1649=EDGE_LOOP ( 'NONE', ( #2501, #360, #4742 ) ) ;
#1650=CARTESIAN_POINT ( 'NONE',  ( -4.207491450040567571, 2.029819825146470524, -3.671670828759566074 ) ) ;
#1652=EDGE_CURVE ( 'NONE', #7956, #2382, #7598, .T. ) ;
#1669=CARTESIAN_POINT ( 'NONE',  ( 1.411581201560190495E-15, 4.862606272033091592, -3.745885042887436622 ) ) ;
#1676=CARTESIAN_POINT ( 'NONE',  ( -4.140404888673278272, -2.228338276487456415, -3.686887068327035166 ) ) ;
#1677=CARTESIAN_POINT ( 'NONE',  ( -4.204114297095464359, 1.660363174096617156, -3.602136431857887011 ) ) ;
#1697=DIRECTION ( 'NONE',  ( 0.000000000000000000, -1.000000000000000000, 0.000000000000000000 ) ) ;
#1698=ORIENTED_EDGE ( 'NONE', *, *, #2070, .F. ) ;
#1723=CARTESIAN_POINT ( 'NONE',  ( -4.211399284164270895, 2.459729995988205964, -3.751162237960538715 ) ) ;
#1728=AXIS2_PLACEMENT_3D ( 'NONE', #1546, #8132, #7462 ) ;
#1742=CARTESIAN_POINT ( 'NONE',  ( 4.000000000000000000, -1.084202172485504434E-14, -3.142992957459231906 ) ) ;
#1755=ORIENTED_EDGE ( 'NONE', *, *, #172, .T. ) ;
#1756=CARTESIAN_POINT ( 'NONE',  ( 1.287237434362044075, 3.875615274277557809, -3.430618716626812059 ) ) ;
#1758=ADVANCED_FACE ( 'NONE', ( #1073 ), #502, .F. ) ;
#1766=B_SPLINE_CURVE_WITH_KNOTS ( 'NONE', 3,
 ( #5531, #7587, #4183, #885, #217, #8203, #2233, #1669 ),
 .UNSPECIFIED., .F., .F.,
 ( 4, 2, 2, 4 ),
 ( 0.000000000000000000, 0.002450665683189820997, 0.003675998524784731495, 0.004901331366379641993 ),
 .UNSPECIFIED. ) ;
#1785=B_SPLINE_CURVE_WITH_KNOTS ( 'NONE', 3,
 ( #5837, #7858, #8512, #6301, #1902, #291 ),
 .UNSPECIFIED., .F., .F.,
 ( 4, 2, 4 ),
 ( 0.000000000000000000, 0.0002095117440854730670, 0.0004190234881709461339 ),
 .UNSPECIFIED. ) ;
#1787=CARTESIAN_POINT ( 'NONE',  ( 4.000000000000000888, 1.539600717838996990, -3.300726591567079815 ) ) ;
#1800=ADVANCED_FACE ( 'NONE', ( #3815 ), #4116, .T. ) ;
#1804=CARTESIAN_POINT ( 'NONE',  ( -0.3208286057739654917, 4.433571671609680465, -0.3503314178412548774 ) ) ;
#1814=DIRECTION ( 'NONE',  ( -1.000000000000000000, 0.000000000000000000, 0.000000000000000000 ) ) ;
#1822=ORIENTED_EDGE ( 'NONE', *, *, #1315, .F. ) ;
#1827=CARTESIAN_POINT ( 'NONE',  ( 4.211140560182196957, -2.431303136016555122, -3.745885042887436622 ) ) ;
#1850=CARTESIAN_POINT ( 'NONE',  ( 0.000000000000000000, 0.000000000000000000, -4.000000000000000000 ) ) ;
#1862=ORIENTED_EDGE ( 'NONE', *, *, #2022, .T. ) ;
#1865=CARTESIAN_POINT ( 'NONE',  ( -2.100000000000000089, 2.571758278209441957E-16, -5.000000000000000000 ) ) ;
#1871=AXIS2_PLACEMENT_3D ( 'NONE', #2575, #1298, #648 ) ;
#1873=CARTESIAN_POINT ( 'NONE',  ( -4.000000000000000000, -1.560351142792950618, -0.2242961665059814425 ) ) ;
#1875=DIRECTION ( 'NONE',  ( -1.000000000000000000, 0.000000000000000000, 0.000000000000000000 ) ) ;
#1887=ORIENTED_EDGE ( 'NONE', *, *, #3719, .F. ) ;
#1891=DIRECTION ( 'NONE',  ( -1.000000000000000000, 0.000000000000000000, 0.000000000000000000 ) ) ;
#1902=CARTESIAN_POINT ( 'NONE',  ( 4.154306624731137099, 2.398490048084935822, -3.721999068284414847 ) ) ;
#1908=CARTESIAN_POINT ( 'NONE',  ( 1.567478505476134606E-15, 4.618802153517012066, -3.433295621305382905 ) ) ;
#1921=B_SPLINE_CURVE_WITH_KNOTS ( 'NONE', 3,
 ( #7787, #2356, #1082, #7661, #423, #1827 ),
 .UNSPECIFIED., .F., .F.,
 ( 4, 2, 4 ),
 ( 0.002452478801916361129, 0.003676905084148001344, 0.004901331366379641126 ),
 .UNSPECIFIED. ) ;
#1923=CARTESIAN_POINT ( 'NONE',  ( -4.000000000000000000, -2.309401076758512694, -5.000000000000000000 ) ) ;
#1925=FACE_OUTER_BOUND ( 'NONE', #4951, .T. ) ;
#1936=VECTOR ( 'NONE', #6086, 1000.000000000000114 ) ;
#1945=CARTESIAN_POINT ( 'NONE',  ( -4.000000000000000000, 0.000000000000000000, 0.000000000000000000 ) ) ;
#1956=CARTESIAN_POINT ( 'NONE',  ( 4.197393957002303999, 7.772902908466098641E-14, -3.503767560748929810 ) ) ;
#1960=ORIENTED_EDGE ( 'NONE', *, *, #8465, .F. ) ;
#1963=CARTESIAN_POINT ( 'NONE',  ( 4.211399257449709665, -2.459727064652517114, -3.751161691472417736 ) ) ;
#1969=DIRECTION ( 'NONE',  ( -1.000000000000000000, 0.000000000000000000, 0.000000000000000000 ) ) ;
#1976=AXIS2_PLACEMENT_3D ( 'NONE', #2550, #536, #7773 ) ;
#1991=CIRCLE ( 'NONE', #735, 2.100000000000000089 ) ;
#2009=AXIS2_PLACEMENT_3D ( 'NONE', #717, #3029, #3115 ) ;
#2010=CARTESIAN_POINT ( 'NONE',  ( 4.000000000000000000, 2.512223110932545023, -3.469391141908803711 ) ) ;
#2014=FACE_OUTER_BOUND ( 'NONE', #2995, .T. ) ;
#2015=VECTOR ( 'NONE', #5613, 999.9999999999998863 ) ;
#2022=EDGE_CURVE ( 'NONE', #1026, #7552, #105, .T. ) ;
#2024=CARTESIAN_POINT ( 'NONE',  ( 4.000000000000003553, -2.309401076758513138, -3.504271511726786859 ) ) ;
#2029=EDGE_LOOP ( 'NONE', ( #7948, #4445, #4555, #5, #8067 ) ) ;
#2030=( LENGTH_UNIT ( ) NAMED_UNIT ( * ) SI_UNIT ( .MILLI., .METRE. ) );
#2037=VECTOR ( 'NONE', #5205, 1000.000000000000000 ) ;
#2041=EDGE_LOOP ( 'NONE', ( #4308, #5411, #1252, #4808, #5569 ) ) ;
#2051=LINE ( 'NONE', #1923, #4371 ) ;
#2053=CARTESIAN_POINT ( 'NONE',  ( 4.000000000000000000, 1.680228229147133767, -3.316631783032546021 ) ) ;
#2059=DIRECTION ( 'NONE',  ( 0.000000000000000000, 0.000000000000000000, 1.000000000000000000 ) ) ;
#2061=ADVANCED_FACE ( 'NONE', ( #6711, #764 ), #6849, .T. ) ;
#2070=EDGE_CURVE ( 'NONE', #4673, #4209, #5090, .T. ) ;
#2092=FACE_OUTER_BOUND ( 'NONE', #2401, .T. ) ;
#2097=EDGE_CURVE ( 'NONE', #392, #8131, #8166, .T. ) ;
#2100=CARTESIAN_POINT ( 'NONE',  ( -4.211140560182196957, 2.431303136016537803, -3.745885042887433514 ) ) ;
#2101=ADVANCED_FACE ( 'NONE', ( #6145 ), #3501, .T. ) ;
#2133=FACE_OUTER_BOUND ( 'NONE', #5563, .T. ) ;
#2142=CARTESIAN_POINT ( 'NONE',  ( -2.000000000000006661, 3.464101615137750834, 0.000000000000000000 ) ) ;
#2153=ADVANCED_FACE ( 'NONE', ( #7062 ), #4269, .T. ) ;
#2155=CARTESIAN_POINT ( 'NONE',  ( 4.000000000000000000, -1.942223658245635809, -0.3516579909967643691 ) ) ;
#2161=ORIENTED_EDGE ( 'NONE', *, *, #3865, .T. ) ;
#2164=CARTESIAN_POINT ( 'NONE',  ( 3.511755186886750923, -2.826662030176382956, -3.597382984111582083 ) ) ;
#2165=CARTESIAN_POINT ( 'NONE',  ( 0.000000000000000000, 0.000000000000000000, 0.000000000000000000 ) ) ;
#2168=EDGE_LOOP ( 'NONE', ( #8562, #5106, #3391, #4728 ) ) ;
#2184=CARTESIAN_POINT ( 'NONE',  ( -0.5469614295416921346, 4.303013824936271270, -3.535263753543735454 ) ) ;
#2185=LINE ( 'NONE', #5526, #2015 ) ;
#2194=ADVANCED_FACE ( 'NONE', ( #2338 ), #584, .F. ) ;
#2198=CARTESIAN_POINT ( 'NONE',  ( -1.390230914382372118, -4.043987460488664532, -3.502507215260523665 ) ) ;
#2200=VERTEX_POINT ( 'NONE', #5960 ) ;
#2205=FACE_OUTER_BOUND ( 'NONE', #2168, .T. ) ;
#2208=CARTESIAN_POINT ( 'NONE',  ( -6.473970235329672780E-16, -4.862606272033106691, -3.745885042887442395 ) ) ;
#2217=CARTESIAN_POINT ( 'NONE',  ( -6.473970235329672780E-16, -4.862606272033106691, -3.745885042887442395 ) ) ;
#2218=CARTESIAN_POINT ( 'NONE',  ( -0.6920835326022555245, -4.454600218803899558, -3.597382984111586079 ) ) ;
#2220=CARTESIAN_POINT ( 'NONE',  ( 3.455068668934414777, -2.624017327439094327, -3.316620875263732504 ) ) ;
#2223=CARTESIAN_POINT ( 'NONE',  ( 0.000000000000000000, 0.000000000000000000, -0.3080913168122742518 ) ) ;
#2231=CARTESIAN_POINT ( 'NONE',  ( -2.000000000000007550, -3.464101615137749945, 0.000000000000000000 ) ) ;
#2233=CARTESIAN_POINT ( 'NONE',  ( -0.3461262719736137305, 4.658553426539289610, -3.671615880910373608 ) ) ;
#2234=AXIS2_PLACEMENT_3D ( 'NONE', #3612, #384, #8364 ) ;
#2243=CARTESIAN_POINT ( 'NONE',  ( 4.000000000000000000, -2.309401076758516691, -0.4999999999999995559 ) ) ;
#2261=CARTESIAN_POINT ( 'NONE',  ( -1.999999999999999556, 3.464101615137754830, -3.142992957459232795 ) ) ;
#2273=CARTESIAN_POINT ( 'NONE',  ( 0.000000000000000000, 0.000000000000000000, 3.469446951953614189E-15 ) ) ;
#2275=CARTESIAN_POINT ( 'NONE',  ( -1.360585162435467455, 4.061296242128285883, -3.505054077164959203 ) ) ;
#2302=B_SPLINE_CURVE_WITH_KNOTS ( 'NONE', 3,
 ( #1945, #3078, #3248, #4505, #6422, #4586, #5721, #465 ),
 .UNSPECIFIED., .F., .F.,
 ( 4, 2, 2, 4 ),
 ( 0.005725059856848641743, 0.006314084072593626612, 0.006903108288338611481, 0.008081156719828581220 ),
 .UNSPECIFIED. ) ;
#2327=CIRCLE ( 'NONE', #3563, 4.000000000000000000 ) ;
#2332=CARTESIAN_POINT ( 'NONE',  ( -3.349226789952655547, -2.685125164760744809, -0.2236248678334863682 ) ) ;
#2337=CARTESIAN_POINT ( 'NONE',  ( -4.235886605889389145, -2.417314728048544303, -3.751161874094020909 ) ) ;
#2338=FACE_OUTER_BOUND ( 'NONE', #2029, .T. ) ;
#2352=EDGE_LOOP ( 'NONE', ( #7732, #7134, #4112, #7783 ) ) ;
#2356=CARTESIAN_POINT ( 'NONE',  ( 4.197393957002303999, -0.4069871074557456780, -3.503767560748925813 ) ) ;
#2380=CARTESIAN_POINT ( 'NONE',  ( -2.836893136758495970, -3.208949435745868328, -3.505054077164885484 ) ) ;
#2381=CARTESIAN_POINT ( 'NONE',  ( -4.000000000000000000, -2.472261339043343220, -3.687027428081192326 ) ) ;
#2382=VERTEX_POINT ( 'NONE', #6573 ) ;
#2385=CARTESIAN_POINT ( 'NONE',  ( 2.687328764639642653, -3.067272167851299969, -0.05923475698271395140 ) ) ;
#2399=CARTESIAN_POINT ( 'NONE',  ( 3.999999999999999112, -1.539600717839012978, -3.300726591567080703 ) ) ;
#2401=EDGE_LOOP ( 'NONE', ( #2161, #1516, #1755, #3546 ) ) ;
#2402=CARTESIAN_POINT ( 'NONE',  ( 0.000000000000000000, 0.000000000000000000, -25.03750572909317285 ) ) ;
#2422=DIRECTION ( 'NONE',  ( 0.000000000000000000, 0.000000000000000000, 1.000000000000000000 ) ) ;
#2438=DIRECTION ( 'NONE',  ( -1.000000000000000000, 0.000000000000000000, 0.000000000000000000 ) ) ;
#2442=ORIENTED_EDGE ( 'NONE', *, *, #5342, .F. ) ;
#2453=CARTESIAN_POINT ( 'NONE',  ( 4.000000000000000000, -2.309401076758514915, -3.433295621305383349 ) ) ;
#2457=ORIENTED_EDGE ( 'NONE', *, *, #7174, .F. ) ;
#2459=AXIS2_PLACEMENT_3D ( 'NONE', #5476, #2909, #8231 ) ;
#2483=CARTESIAN_POINT ( 'NONE',  ( 2.500000000000000888, 3.061616997868384127E-16, -4.974599999999998801 ) ) ;
#2485=EDGE_CURVE ( 'NONE', #1044, #3408, #168, .T. ) ;
#2487=CARTESIAN_POINT ( 'NONE',  ( -4.000000000000000000, -2.309401076758515803, -0.4999999999999995559 ) ) ;
#2501=ORIENTED_EDGE ( 'NONE', *, *, #8465, .T. ) ;
#2502=CARTESIAN_POINT ( 'NONE',  ( 0.6810597143197052450, 4.461075778259290914, -3.598441714920602053 ) ) ;
#2524=EDGE_CURVE ( 'NONE', #4773, #7074, #883, .T. ) ;
#2525=DIRECTION ( 'NONE',  ( -0.000000000000000000, 0.000000000000000000, -1.000000000000000000 ) ) ;
#2541=CARTESIAN_POINT ( 'NONE',  ( 3.453038570460273071, 2.625189405340834448, -3.535263753543585352 ) ) ;
#2550=CARTESIAN_POINT ( 'NONE',  ( 0.000000000000000000, 0.000000000000000000, 0.000000000000000000 ) ) ;
#2564=CARTESIAN_POINT ( 'NONE',  ( 0.000000000000000000, 0.000000000000000000, 0.000000000000000000 ) ) ;
#2569=CARTESIAN_POINT ( 'NONE',  ( 4.197393957002303999, 0.8151795401431359833, -3.503767560748935139 ) ) ;
#2572=CARTESIAN_POINT ( 'NONE',  ( -0.6448876103708541807, -4.246476118072358474, -0.2256878752776773356 ) ) ;
#2573=VERTEX_POINT ( 'NONE', #2231 ) ;
#2574=ORIENTED_EDGE ( 'NONE', *, *, #2097, .F. ) ;
#2575=CARTESIAN_POINT ( 'NONE',  ( 8.673617379884035472E-16, 4.618802153517012954, 0.000000000000000000 ) ) ;
#2590=CARTESIAN_POINT ( 'NONE',  ( 4.000000000000000000, 0.000000000000000000, 0.000000000000000000 ) ) ;
#2615=CARTESIAN_POINT ( 'NONE',  ( 1.655952806101427033, -3.662737355149048302, -1.182683869819604841E-14 ) ) ;
#2624=CARTESIAN_POINT ( 'NONE',  ( -4.000000000000000000, 2.309401076758498483, -3.433295621305379353 ) ) ;
#2648=CIRCLE ( 'NONE', #275, 4.000000000000000000 ) ;
#2652=EDGE_LOOP ( 'NONE', ( #2850, #3633 ) ) ;
#2655=CARTESIAN_POINT ( 'NONE',  ( 4.197310751797292738, 0.8178363989516252985, -3.502498386812444409 ) ) ;
#2656=CARTESIAN_POINT ( 'NONE',  ( 0.000000000000000000, 0.000000000000000000, -4.000000000000000000 ) ) ;
#2676=DIRECTION ( 'NONE',  ( -0.000000000000000000, -0.000000000000000000, 1.000000000000000000 ) ) ;
#2699=FACE_BOUND ( 'NONE', #6652, .T. ) ;
#2704=CARTESIAN_POINT ( 'NONE',  ( 4.000000000000000000, -2.471525695159793035, -3.686886880705770864 ) ) ;
#2705=DIRECTION ( 'NONE',  ( -0.000000000000000000, -0.000000000000000000, 1.000000000000000000 ) ) ;
#2711=ADVANCED_FACE ( 'NONE', ( #486 ), #3143, .T. ) ;
#2715=ORIENTED_EDGE ( 'NONE', *, *, #6850, .F. ) ;
#2745=CARTESIAN_POINT ( 'NONE',  ( -4.197393957002303999, -7.773935952363655451E-14, -3.503767560748929810 ) ) ;
#2757=CARTESIAN_POINT ( 'NONE',  ( 4.000000000000000000, -2.309401076758514915, -3.433295621305383349 ) ) ;
#2761=DIRECTION ( 'NONE',  ( 1.000000000000000000, 0.000000000000000000, 0.000000000000000000 ) ) ;
#2770=( LENGTH_UNIT ( ) NAMED_UNIT ( * ) SI_UNIT ( .MILLI., .METRE. ) );
#2772=EDGE_LOOP ( 'NONE', ( #8362, #8413, #901, #8135, #6291 ) ) ;
#2775=FACE_OUTER_BOUND ( 'NONE', #3187, .T. ) ;
#2781=CARTESIAN_POINT ( 'NONE',  ( -4.101948962585905356, -2.368261337751088824, -3.681124513963624167 ) ) ;
#2790=CARTESIAN_POINT ( 'NONE',  ( -2.345747346278108214, 3.264484291692489215, -0.01223254789873409049 ) ) ;
#2792=ADVANCED_FACE ( 'NONE', ( #4047 ), #535, .T. ) ;
#2801=DIRECTION ( 'NONE',  ( 0.8660254037844379305, 0.5000000000000013323, 0.000000000000000000 ) ) ;
#2806=FACE_OUTER_BOUND ( 'NONE', #6015, .T. ) ;
#2808=ADVANCED_FACE ( 'NONE', ( #562 ), #6604, .F. ) ;
#2819=EDGE_LOOP ( 'NONE', ( #1862, #22, #3504 ) ) ;
#2833=CARTESIAN_POINT ( 'NONE',  ( -2.100000000000000089, 2.571758278209441957E-16, -0.2800830152838844622 ) ) ;
#2847=EDGE_CURVE ( 'NONE', #2893, #2382, #4696, .T. ) ;
#2848=CARTESIAN_POINT ( 'NONE',  ( -0.5636800770129166693, -4.293361309317430319, -3.531542292955206275 ) ) ;
#2850=ORIENTED_EDGE ( 'NONE', *, *, #4226, .T. ) ;
#2867=CARTESIAN_POINT ( 'NONE',  ( -4.000000000000000000, 2.309401076758498483, -3.433295621305379353 ) ) ;
#2870=CARTESIAN_POINT ( 'NONE',  ( 2.712762565639649015, -3.052587955997662306, -3.430618716626630871 ) ) ;
#2871=ORIENTED_EDGE ( 'NONE', *, *, #6403, .T. ) ;
#2872=AXIS2_PLACEMENT_3D ( 'NONE', #3414, #805, #6057 ) ;
#2874=CARTESIAN_POINT ( 'NONE',  ( -4.203833317240879275, -1.627343821129593859, -3.597273115243890818 ) ) ;
#2876=CARTESIAN_POINT ( 'NONE',  ( -3.455068668934486276, 2.624017327439035707, -3.316620875263955437 ) ) ;
#2881=ORIENTED_EDGE ( 'NONE', *, *, #5342, .T. ) ;
#2883=( NAMED_UNIT ( * ) PLANE_ANGLE_UNIT ( ) SI_UNIT ( $, .RADIAN. ) );
#2891=ORIENTED_EDGE ( 'NONE', *, *, #6850, .T. ) ;
#2893=VERTEX_POINT ( 'NONE', #2745 ) ;
#2895=EDGE_CURVE ( 'NONE', #1258, #5075, #7893, .T. ) ;
#2897=B_SPLINE_CURVE_WITH_KNOTS ( 'NONE', 3,
 ( #5670, #6144, #7685, #5015, #1586, #6848 ),
 .UNSPECIFIED., .F., .F.,
 ( 4, 2, 4 ),
 ( 0.002365888236227995517, 0.003551327329835084114, 0.004736766423442172712 ),
 .UNSPECIFIED. ) ;
#2909=DIRECTION ( 'NONE',  ( -0.000000000000000000, -0.000000000000000000, 1.000000000000000000 ) ) ;
#2911=CARTESIAN_POINT ( 'NONE',  ( 4.211140560182196957, 2.431303136016536470, -3.745885042887433514 ) ) ;
#2912=ORIENTED_EDGE ( 'NONE', *, *, #7519, .F. ) ;
#2917=FACE_OUTER_BOUND ( 'NONE', #4200, .T. ) ;
#2919=CIRCLE ( 'NONE', #6805, 2.500000000000000444 ) ;
#2920=DIRECTION ( 'NONE',  ( -0.000000000000000000, -0.000000000000000000, 1.000000000000000000 ) ) ;
#2928=DIRECTION ( 'NONE',  ( 0.000000000000000000, 0.000000000000000000, 1.000000000000000000 ) ) ;
#2933=ADVANCED_FACE ( 'NONE', ( #6870 ), #8105, .T. ) ;
#2959=EDGE_LOOP ( 'NONE', ( #3998, #1522, #3558, #8219 ) ) ;
#2962=CONICAL_SURFACE ( 'NONE', #3106, 5.560781378645573980, 1.221730476396046816 ) ;
#2972=SURFACE_STYLE_FILL_AREA ( #6183 ) ;
#2975=ADVANCED_FACE ( 'NONE', ( #2133 ), #7094, .F. ) ;
#2980=DIRECTION ( 'NONE',  ( 1.000000000000000000, 0.000000000000000000, 0.000000000000000000 ) ) ;
#2986=CARTESIAN_POINT ( 'NONE',  ( -6.259644161404862988E-16, -4.618802153517027165, -3.504271511726793076 ) ) ;
#2991=ORIENTED_EDGE ( 'NONE', *, *, #7865, .F. ) ;
#2995=EDGE_LOOP ( 'NONE', ( #987, #5201, #2457, #3126 ) ) ;
#3000=EDGE_LOOP ( 'NONE', ( #6420, #5647, #2881, #746 ) ) ;
#3008=CARTESIAN_POINT ( 'NONE',  ( 1.999999999999998224, -3.464101615137772594, -3.142992957459239012 ) ) ;
#3009=EDGE_CURVE ( 'NONE', #7420, #1514, #4662, .T. ) ;
#3010=EDGE_CURVE ( 'NONE', #3609, #1026, #7042, .T. ) ;
#3011=CONICAL_SURFACE ( 'NONE', #3561, 2.500000000000000888, 0.9599310885968785900 ) ;
#3023=CARTESIAN_POINT ( 'NONE',  ( 1.734723475976807094E-15, 4.618802153517012954, -0.4999999999999995559 ) ) ;
#3024=CARTESIAN_POINT ( 'NONE',  ( -4.000000000000000000, 1.700094919196744270, -3.320312364301766017 ) ) ;
#3025=EDGE_CURVE ( 'NONE', #6857, #8131, #5256, .T. ) ;
#3029=DIRECTION ( 'NONE',  ( 0.000000000000000000, 0.000000000000000000, 1.000000000000000000 ) ) ;
#3065=PLANE ( 'NONE',  #8113 ) ;
#3071=CARTESIAN_POINT ( 'NONE',  ( 3.680118525130245732, -2.494084732383344605, -0.3507732604232533524 ) ) ;
#3076=DIRECTION ( 'NONE',  ( 1.000000000000000000, 0.000000000000000000, 0.000000000000000000 ) ) ;
#3078=CARTESIAN_POINT ( 'NONE',  ( -4.000000000000000000, 0.1981133338132459731, 2.096406544454392723E-17 ) ) ;
#3085=CARTESIAN_POINT ( 'NONE',  ( -4.000000000000000000, -0.7890432684750890990, -0.04868663549882315533 ) ) ;
#3086=ORIENTED_EDGE ( 'NONE', *, *, #2847, .F. ) ;
#3097=CARTESIAN_POINT ( 'NONE',  ( 1.567478505476134606E-15, 4.618802153517012066, -3.433295621305382905 ) ) ;
#3104=CARTESIAN_POINT ( 'NONE',  ( 4.140404888673277384, 2.228338276487440428, -3.686887068327033390 ) ) ;
#3106=AXIS2_PLACEMENT_3D ( 'NONE', #4902, #1379, #4729 ) ;
#3115=DIRECTION ( 'NONE',  ( 1.000000000000000000, 0.000000000000000000, 0.000000000000000000 ) ) ;
#3119=EDGE_CURVE ( 'NONE', #917, #5075, #1785, .T. ) ;
#3123=CARTESIAN_POINT ( 'NONE',  ( 0.000000000000000000, 0.000000000000000000, 0.000000000000000000 ) ) ;
#3126=ORIENTED_EDGE ( 'NONE', *, *, #3802, .F. ) ;
#3127=VERTEX_POINT ( 'NONE', #1235 ) ;
#3141=B_SPLINE_CURVE_WITH_KNOTS ( 'NONE', 3,
 ( #1372, #5895, #718, #5159, #8564, #3952, #6674, #7164 ),
 .UNSPECIFIED., .F., .F.,
 ( 4, 2, 2, 4 ),
 ( 2.465131517075058656E-07, 0.001183067374689851080, 0.001774477805458923299, 0.002365888236227995517 ),
 .UNSPECIFIED. ) ;
#3142=CARTESIAN_POINT ( 'NONE',  ( 4.000000000000000000, 2.309401076758497151, -3.433295621305379353 ) ) ;
#3143=PLANE ( 'NONE',  #3182 ) ;
#3176=CARTESIAN_POINT ( 'NONE',  ( -2.688821387764050996E-14, -4.618802153517012954, -0.4999999999999995559 ) ) ;
#3182=AXIS2_PLACEMENT_3D ( 'NONE', #3838, #3746, #4444 ) ;
#3187=EDGE_LOOP ( 'NONE', ( #2574, #1648, #6032, #6934, #7249, #4325, #982 ) ) ;
#3188=CARTESIAN_POINT ( 'NONE',  ( 2.836893136758676270, 3.208949435745843903, -3.505054077164911241 ) ) ;
#3189=CIRCLE ( 'NONE', #5261, 2.100000000000000089 ) ;
#3201=CARTESIAN_POINT ( 'NONE',  ( 4.000000000000000000, 0.9868501483902631932, -0.09357334158579604100 ) ) ;
#3203=EDGE_CURVE ( 'NONE', #6725, #4773, #3189, .T. ) ;
#3220=CARTESIAN_POINT ( 'NONE',  ( -4.000000000000000000, -7.806255641895631925E-15, -3.142992957459232350 ) ) ;
#3235=CARTESIAN_POINT ( 'NONE',  ( 4.211140560182196957, -2.431303136016555122, -3.745885042887436622 ) ) ;
#3243=CARTESIAN_POINT ( 'NONE',  ( 4.211140560182196957, -2.431303136016555122, -3.745885042887436622 ) ) ;
#3248=CARTESIAN_POINT ( 'NONE',  ( -4.000000000000000000, 0.3987449864459974846, -0.01220643443059782861 ) ) ;
#3254=PRODUCT_DEFINITION_CONTEXT ( 'detailed design', #8095, 'design' ) ;
#3257=DIRECTION ( 'NONE',  ( 1.000000000000000000, 0.000000000000000000, 0.000000000000000000 ) ) ;
#3287=ORIENTED_EDGE ( 'NONE', *, *, #7271, .T. ) ;
#3297=DIRECTION ( 'NONE',  ( -0.000000000000000000, -0.000000000000000000, 1.000000000000000000 ) ) ;
#3302=CARTESIAN_POINT ( 'NONE',  ( -2.000000000000007550, -3.464101615137749945, 0.000000000000000000 ) ) ;
#3329=EDGE_CURVE ( 'NONE', #4775, #5858, #2897, .T. ) ;
#3334=B_SPLINE_CURVE_WITH_KNOTS ( 'NONE', 3,
 ( #2590, #6582, #579, #5233, #3201, #6536, #5317, #6460 ),
 .UNSPECIFIED., .F., .F.,
 ( 4, 2, 2, 4 ),
 ( 0.005725059856848645212, 0.006314084072593634418, 0.006903108288338624492, 0.008081156719828603771 ),
 .UNSPECIFIED. ) ;
#3337=AXIS2_PLACEMENT_3D ( 'NONE', #1850, #493, #5708 ) ;
#3342=DIRECTION ( 'NONE',  ( -1.000000000000000000, 0.000000000000000000, 0.000000000000000000 ) ) ;
#3350=ADVANCED_FACE ( 'NONE', ( #4188 ), #5035, .F. ) ;
#3371=VERTEX_POINT ( 'NONE', #6890 ) ;
#3373=CIRCLE ( 'NONE', #312, 2.499999999999999556 ) ;
#3391=ORIENTED_EDGE ( 'NONE', *, *, #7271, .F. ) ;
#3399=CARTESIAN_POINT ( 'NONE',  ( -5.560781378645573980, 0.000000000000000000, -4.000000000000000000 ) ) ;
#3408=VERTEX_POINT ( 'NONE', #3023 ) ;
#3410=CARTESIAN_POINT ( 'NONE',  ( -2.100000000000000089, 2.571758278209441957E-16, -4.694516984716113228 ) ) ;
#3414=CARTESIAN_POINT ( 'NONE',  ( 8.673617379884035472E-16, 4.618802153517012954, -5.000000000000000000 ) ) ;
#3428=CARTESIAN_POINT ( 'NONE',  ( 1.747541505913279281, -3.837784562140273081, -3.503702292528912299 ) ) ;
#3437=CARTESIAN_POINT ( 'NONE',  ( 1.567478505476135000E-15, 4.618802153517012954, -3.504269196027527844 ) ) ;
#3440=CARTESIAN_POINT ( 'NONE',  ( 1.360585162435110629, -4.061296242128317857, -3.505054077164905024 ) ) ;
#3449=ORIENTED_EDGE ( 'NONE', *, *, #6795, .T. ) ;
#3450=CARTESIAN_POINT ( 'NONE',  ( -4.024497503033519941, 2.323544716729375459, -3.572167766733379768 ) ) ;
#3459=CARTESIAN_POINT ( 'NONE',  ( 3.999999999999999112, -0.3979232138631231819, -5.929230630780099908E-17 ) ) ;
#3480=DIRECTION ( 'NONE',  ( -1.000000000000000000, 0.000000000000000000, 0.000000000000000000 ) ) ;
#3483=CARTESIAN_POINT ( 'NONE',  ( 1.257172072275274388, -3.892973519170983110, -3.433252694550781303 ) ) ;
#3484=ORIENTED_EDGE ( 'NONE', *, *, #6080, .T. ) ;
#3501=PLANE ( 'NONE',  #8025 ) ;
#3504=ORIENTED_EDGE ( 'NONE', *, *, #7, .F. ) ;
#3524=CARTESIAN_POINT ( 'NONE',  ( 1.411581201560190495E-15, 4.862606272033091592, -3.745885042887436622 ) ) ;
#3525=CARTESIAN_POINT ( 'NONE',  ( 0.6920835326022565237, 4.454600218803884459, -3.597382984111579862 ) ) ;
#3530=CARTESIAN_POINT ( 'NONE',  ( 2.100000000000000089, 0.000000000000000000, -5.000000000000000000 ) ) ;
#3546=ORIENTED_EDGE ( 'NONE', *, *, #3856, .F. ) ;
#3558=ORIENTED_EDGE ( 'NONE', *, *, #880, .F. ) ;
#3561=AXIS2_PLACEMENT_3D ( 'NONE', #4899, #8220, #812 ) ;
#3563=AXIS2_PLACEMENT_3D ( 'NONE', #2165, #7429, #194 ) ;
#3567=CARTESIAN_POINT ( 'NONE',  ( 4.141042297810615835, -2.227970268150433863, -3.687027686973623819 ) ) ;
#3578=CARTESIAN_POINT ( 'NONE',  ( -2.688821387764050996E-14, -4.618802153517012954, -0.4999999999999995559 ) ) ;
#3590=ORIENTED_EDGE ( 'NONE', *, *, #3119, .T. ) ;
#3596=EDGE_CURVE ( 'NONE', #926, #3371, #4874, .T. ) ;
#3599=ORIENTED_EDGE ( 'NONE', *, *, #7, .T. ) ;
#3603=ORIENTED_EDGE ( 'NONE', *, *, #4936, .T. ) ;
#3607=CARTESIAN_POINT ( 'NONE',  ( -3.510273485745307287, -2.827716139362669967, -3.610536846335890004 ) ) ;
#3609=VERTEX_POINT ( 'NONE', #2757 ) ;
#3612=CARTESIAN_POINT ( 'NONE',  ( 0.000000000000000000, 0.000000000000000000, -0.2800830152838844622 ) ) ;
#3619=EDGE_LOOP ( 'NONE', ( #7531, #8300, #5892, #1211, #1027 ) ) ;
#3633=ORIENTED_EDGE ( 'NONE', *, *, #2070, .T. ) ;
#3635=EDGE_CURVE ( 'NONE', #6857, #7956, #8482, .T. ) ;
#3654=ORIENTED_EDGE ( 'NONE', *, *, #2097, .T. ) ;
#3667=SURFACE_SIDE_STYLE ('',( #2972 ) ) ;
#3669=CARTESIAN_POINT ( 'NONE',  ( 1.274258131564866448, 3.883108878240963513, -3.220599429844046568 ) ) ;
#3676=CARTESIAN_POINT ( 'NONE',  ( -3.453038570459499024, -2.625189405340453419, -3.535263753545272891 ) ) ;
#3677=CARTESIAN_POINT ( 'NONE',  ( -4.000000000000000000, -0.8382240730041925492, -3.220610619767135141 ) ) ;
#3678=VECTOR ( 'NONE', #5048, 1000.000000000000000 ) ;
#3681=CARTESIAN_POINT ( 'NONE',  ( 3.355112389629172576, -2.681727112203168950, -0.2256878752776777242 ) ) ;
#3682=CARTESIAN_POINT ( 'NONE',  ( -1.240299975428113101E-15, -4.647091401871173311, -3.572172305156514849 ) ) ;
#3688=ORIENTED_EDGE ( 'NONE', *, *, #880, .T. ) ;
#3711=CARTESIAN_POINT ( 'NONE',  ( 0.5636800770130377947, 4.293361309317166530, -3.531542292954102713 ) ) ;
#3714=DIRECTION ( 'NONE',  ( -0.000000000000000000, -0.000000000000000000, 1.000000000000000000 ) ) ;
#3719=EDGE_CURVE ( 'NONE', #7552, #1114, #5819, .T. ) ;
#3729=ORIENTED_EDGE ( 'NONE', *, *, #5962, .T. ) ;
#3734=VECTOR ( 'NONE', #4650, 1000.000000000000227 ) ;
#3746=DIRECTION ( 'NONE',  ( -0.5000000000000016653, 0.8660254037844378194, 0.000000000000000000 ) ) ;
#3759=CARTESIAN_POINT ( 'NONE',  ( -4.211405944401398038, -2.460460786169389902, -3.751298493805494072 ) ) ;
#3778=B_SPLINE_CURVE_WITH_KNOTS ( 'NONE', 3,
 ( #5689, #2399, #1742, #1787, #4389 ),
 .UNSPECIFIED., .F., .F.,
 ( 4, 1, 4 ),
 ( 0.000000000000000000, 0.002309401076758505790, 0.004618802153517011580 ),
 .UNSPECIFIED. ) ;
#3789=CARTESIAN_POINT ( 'NONE',  ( 5.384454397937118664, 0.000000000000000000, -5.000000000000000000 ) ) ;
#3802=EDGE_CURVE ( 'NONE', #926, #1258, #1766, .T. ) ;
#3810=( GEOMETRIC_REPRESENTATION_CONTEXT ( 3 ) GLOBAL_UNCERTAINTY_ASSIGNED_CONTEXT ( ( #7693 ) ) GLOBAL_UNIT_ASSIGNED_CONTEXT ( ( #2030, #2883, #6966 ) ) REPRESENTATION_CONTEXT ( 'NONE', 'WORKASPACE' ) );
#3814=CONICAL_SURFACE ( 'NONE', #1728, 4.000000000000000000, 0.8911886515913786111 ) ;
#3815=FACE_OUTER_BOUND ( 'NONE', #1649, .T. ) ;
#3830=ORIENTED_EDGE ( 'NONE', *, *, #7865, .T. ) ;
#3838=CARTESIAN_POINT ( 'NONE',  ( 1.567478505476134606E-15, 4.618802153517012066, -5.000000000000000000 ) ) ;
#3843=CARTESIAN_POINT ( 'NONE',  ( 2.742827927723449299, 3.035229711104609596, -3.433252694550591233 ) ) ;
#3844=ADVANCED_FACE ( 'NONE', ( #7990 ), #6094, .F. ) ;
#3856=EDGE_CURVE ( 'NONE', #2200, #1490, #1361, .T. ) ;
#3865=EDGE_CURVE ( 'NONE', #2200, #8282, #8077, .T. ) ;
#3886=B_SPLINE_CURVE_WITH_KNOTS ( 'NONE', 3,
 ( #2487, #4511, #1873, #3085, #8318, #8449 ),
 .UNSPECIFIED., .F., .F.,
 ( 4, 2, 4 ),
 ( 0.003358874760055550156, 0.004541967308452096383, 0.005725059856848641743 ),
 .UNSPECIFIED. ) ;
#3899=CARTESIAN_POINT ( 'NONE',  ( -2.000000000000006661, 3.464101615137750834, 0.000000000000000000 ) ) ;
#3902=CARTESIAN_POINT ( 'NONE',  ( 3.333333333333332593, 2.694301256218250007, -3.300726591567078483 ) ) ;
#3906=ADVANCED_FACE ( 'NONE', ( #803 ), #550, .F. ) ;
#3918=CARTESIAN_POINT ( 'NONE',  ( 4.000000000000000000, -1.677850389431204459, -3.535268758346977513 ) ) ;
#3936=AXIS2_PLACEMENT_3D ( 'NONE', #5811, #2525, #1875 ) ;
#3941=VECTOR ( 'NONE', #2059, 1000.000000000000000 ) ;
#3952=CARTESIAN_POINT ( 'NONE',  ( 1.654252653721905331, 3.663718938583014229, -0.01223254789873410957 ) ) ;
#3955=B_SPLINE_CURVE_WITH_KNOTS ( 'NONE', 3,
 ( #6826, #2874, #8192, #8150 ),
 .UNSPECIFIED., .F., .F.,
 ( 4, 4 ),
 ( 0.000000000000000000, 0.002452478801916376308 ),
 .UNSPECIFIED. ) ;
#3956=CARTESIAN_POINT ( 'NONE',  ( 4.000000000000000000, 2.309401076758497151, -5.000000000000000000 ) ) ;
#3957=ORIENTED_EDGE ( 'NONE', *, *, #3802, .T. ) ;
#3967=CARTESIAN_POINT ( 'NONE',  ( 4.000000000000000000, -2.511475576507276042, -3.469253905236643565 ) ) ;
#3983=DIRECTION ( 'NONE',  ( 0.000000000000000000, 0.000000000000000000, 1.000000000000000000 ) ) ;
#3998=ORIENTED_EDGE ( 'NONE', *, *, #3635, .T. ) ;
#3999=CARTESIAN_POINT ( 'NONE',  ( 4.211140560182196957, 2.431303136016536470, -3.745885042887433514 ) ) ;
#4007=CARTESIAN_POINT ( 'NONE',  ( 4.000000000000000000, 2.309401076758497151, -5.000000000000000000 ) ) ;
#4011=CARTESIAN_POINT ( 'NONE',  ( 0.1404048886732821022, 4.699864953788070565, -3.686887068327037387 ) ) ;
#4024=DIRECTION ( 'NONE',  ( 1.000000000000000000, 0.000000000000000000, 0.000000000000000000 ) ) ;
#4036=CIRCLE ( 'NONE', #2234, 2.100000000000000089 ) ;
#4047=FACE_OUTER_BOUND ( 'NONE', #4078, .T. ) ;
#4050=CARTESIAN_POINT ( 'NONE',  ( -0.5276280594146446346, 4.314175951381965746, -3.320322319201721495 ) ) ;
#4067=DIRECTION ( 'NONE',  ( -1.000000000000000000, 0.000000000000000000, 0.000000000000000000 ) ) ;
#4071=UNCERTAINTY_MEASURE_WITH_UNIT (LENGTH_MEASURE( 1.000000000000000082E-05 ), #2770, 'distance_accuracy_value', 'NONE');
#4078=EDGE_LOOP ( 'NONE', ( #778, #3654, #3688, #3086, #3729, #3957, #6902 ) ) ;
#4087=CIRCLE ( 'NONE', #1583, 4.000000000000000000 ) ;
#4091=CARTESIAN_POINT ( 'NONE',  ( -2.500000000000000888, 0.000000000000000000, -4.974599999999998801 ) ) ;
#4093=CARTESIAN_POINT ( 'NONE',  ( 4.000000000000000000, -1.700175430507292473, -3.320327275037661785 ) ) ;
#4094=CARTESIAN_POINT ( 'NONE',  ( -4.000000000000000000, -2.309401076758512694, -5.000000000000000000 ) ) ;
#4101=CARTESIAN_POINT ( 'NONE',  ( -2.171643655288372443, 3.365003104552320767, 2.541098841762897165E-18 ) ) ;
#4112=ORIENTED_EDGE ( 'NONE', *, *, #2524, .T. ) ;
#4116=CONICAL_SURFACE ( 'NONE', #7039, 4.000000000000000000, 0.8911886515913786111 ) ;
#4131=CARTESIAN_POINT ( 'NONE',  ( -3.861362476283256129, -2.629030857716004199, -3.671615880910374941 ) ) ;
#4139=EDGE_CURVE ( 'NONE', #4673, #7074, #8123, .T. ) ;
#4141=CARTESIAN_POINT ( 'NONE',  ( 1.567478505476134606E-15, 4.618802153517012066, -5.000000000000000000 ) ) ;
#4156=DIRECTION ( 'NONE',  ( -1.000000000000000000, 1.224646799147352714E-16, 0.000000000000000000 ) ) ;
#4159=B_SPLINE_CURVE_WITH_KNOTS ( 'NONE', 3,
 ( #5193, #2024, #8509, #7282, #623, #3243 ),
 .UNSPECIFIED., .F., .F.,
 ( 4, 2, 4 ),
 ( 4.336808689942017736E-19, 0.0002095117440854729585, 0.0004190234881709454834 ),
 .UNSPECIFIED. ) ;
#4162=PRODUCT_CONTEXT ( 'NONE', #9, 'mechanical' ) ;
#4171=CARTESIAN_POINT ( 'NONE',  ( 0.5276280594147412240, -4.314175951381924889, -3.320322319201654881 ) ) ;
#4178=CARTESIAN_POINT ( 'NONE',  ( -4.236525694536558362, 2.416953475386465211, -3.751298745799836354 ) ) ;
#4183=CARTESIAN_POINT ( 'NONE',  ( -2.805705207896067144, 3.226868319750155312, -3.503898532754364581 ) ) ;
#4188=FACE_OUTER_BOUND ( 'NONE', #4988, .T. ) ;
#4200=EDGE_LOOP ( 'NONE', ( #6003, #7461, #1222, #8323, #6112 ) ) ;
#4209=VERTEX_POINT ( 'NONE', #4492 ) ;
#4215=CARTESIAN_POINT ( 'NONE',  ( -0.6666666666666651864, 4.233901974057260098, -3.300726591567081147 ) ) ;
#4220=AXIS2_PLACEMENT_3D ( 'NONE', #4387, #7124, #6387 ) ;
#4222=CARTESIAN_POINT ( 'NONE',  ( 0.000000000000000000, 0.000000000000000000, 0.000000000000000000 ) ) ;
#4224=DIRECTION ( 'NONE',  ( 0.000000000000000000, 0.000000000000000000, 1.000000000000000000 ) ) ;
#4226=EDGE_CURVE ( 'NONE', #4209, #4673, #2919, .T. ) ;
#4228=DIRECTION ( 'NONE',  ( 0.8191520442889902442, 1.003171929053522651E-16, -0.5735764363510482688 ) ) ;
#4232=( NAMED_UNIT ( * ) PLANE_ANGLE_UNIT ( ) SI_UNIT ( $, .RADIAN. ) );
#4238=CARTESIAN_POINT ( 'NONE',  ( -2.756197834950067094, -3.027510591568735254, -3.223146290109809797 ) ) ;
#4257=AXIS2_PLACEMENT_3D ( 'NONE', #1508, #8265, #4156 ) ;
#4259=CARTESIAN_POINT ( 'NONE',  ( -1.391697335622809950, -4.043246145443391448, -3.503898532754372575 ) ) ;
#4267=CARTESIAN_POINT ( 'NONE',  ( -1.257172072275743346, 3.892973519171203378, -3.433252694550776862 ) ) ;
#4269=TOROIDAL_SURFACE ( 'NONE', #5513, 5.384454397937118664, 0.5155456020628804703 ) ;
#4280=EDGE_CURVE ( 'NONE', #2382, #8131, #7083, .T. ) ;
#4282=CARTESIAN_POINT ( 'NONE',  ( -4.000000000000000000, -0.8232339106130515116, -3.430630286862743183 ) ) ;
#4299=CARTESIAN_POINT ( 'NONE',  ( -4.211140560182196957, 2.431303136016537803, -3.745885042887433514 ) ) ;
#4304=CARTESIAN_POINT ( 'NONE',  ( 5.384454397937118664, 0.000000000000000000, -4.484454397937119197 ) ) ;
#4308=ORIENTED_EDGE ( 'NONE', *, *, #2485, .F. ) ;
#4324=CARTESIAN_POINT ( 'NONE',  ( -4.197477534772231955, 0.8522413273724368521, -3.505042416683225692 ) ) ;
#4325=ORIENTED_EDGE ( 'NONE', *, *, #2847, .T. ) ;
#4344=DIRECTION ( 'NONE',  ( 0.000000000000000000, 0.000000000000000000, -1.000000000000000000 ) ) ;
#4356=DIRECTION ( 'NONE',  ( -1.000000000000000000, 0.000000000000000000, 0.000000000000000000 ) ) ;
#4371=VECTOR ( 'NONE', #1299, 1000.000000000000000 ) ;
#4372=EDGE_CURVE ( 'NONE', #8282, #2200, #4036, .T. ) ;
#4387=CARTESIAN_POINT ( 'NONE',  ( 0.000000000000000000, 0.000000000000000000, -4.974599999999998801 ) ) ;
#4389=CARTESIAN_POINT ( 'NONE',  ( 4.000000000000000000, 2.309401076758497151, -3.433295621305379353 ) ) ;
#4411=DIRECTION ( 'NONE',  ( 0.000000000000000000, -0.000000000000000000, 1.000000000000000000 ) ) ;
#4413=CARTESIAN_POINT ( 'NONE',  ( -4.000000000000000000, 2.511478553582031203, -3.469254451724764543 ) ) ;
#4426=CARTESIAN_POINT ( 'NONE',  ( -4.197393957002303999, 0.4069871074557429025, -3.503767560748926257 ) ) ;
#4444=DIRECTION ( 'NONE',  ( -0.8660254037844377084, -0.5000000000000015543, 0.000000000000000000 ) ) ;
#4445=ORIENTED_EDGE ( 'NONE', *, *, #5706, .F. ) ;
#4458=DIRECTION ( 'NONE',  ( -0.000000000000000000, -0.000000000000000000, 1.000000000000000000 ) ) ;
#4467=CARTESIAN_POINT ( 'NONE',  ( 4.000000000000000000, 2.309401076758515803, -0.4999999999999995559 ) ) ;
#4478=( BOUNDED_SURFACE ( )  B_SPLINE_SURFACE ( 3, 2, ( 
 ( #3967, #2704, #1963 ),
 ( #4093, #3918, #5346 ),
 ( #1256, #6562, #5296 ),
 ( #4602, #5947, #2655 ),
 ( #2053, #7970, #8060 ),
 ( #2010, #4649, #7308 ) ),
 .UNSPECIFIED., .F., .F., .F. ) 
 B_SPLINE_SURFACE_WITH_KNOTS ( ( 4, 2, 4 ),
 ( 3, 3 ),
 ( 0.02027065861071770947, 0.02273072267836921331, 0.02519078674602071716 ),
 ( 0.000000000000000000, 1.000000000000000000 ),
 .UNSPECIFIED. ) 
 GEOMETRIC_REPRESENTATION_ITEM ( )  RATIONAL_B_SPLINE_SURFACE ( (
 ( 1.000000000000000000, 0.8047781708337304885, 1.000000000000000000),
 ( 1.000000000000000000, 0.8123765190705307671, 1.000000000000000000),
 ( 1.000000000000000000, 0.8190656277163975707, 1.000000000000000000),
 ( 1.000000000000000000, 0.8192366903512159348, 1.000000000000000000),
 ( 1.000000000000000000, 0.8126138454302893610, 1.000000000000000000),
 ( 1.000000000000000000, 0.8047712246031417660, 1.000000000000000000) ) ) 
 REPRESENTATION_ITEM ( '' )  SURFACE ( )  );
#4492=CARTESIAN_POINT ( 'NONE',  ( 2.500000000000000444, 0.000000000000000000, -5.000000000000000888 ) ) ;
#4499=EDGE_CURVE ( 'NONE', #771, #2573, #6820, .T. ) ;
#4505=CARTESIAN_POINT ( 'NONE',  ( -4.000000000000000000, 0.7924765000094600165, -0.05906175389889745803 ) ) ;
#4511=CARTESIAN_POINT ( 'NONE',  ( -4.000000000000000000, -1.942223658245633811, -0.3516579909967644246 ) ) ;
#4524=ORIENTED_EDGE ( 'NONE', *, *, #172, .F. ) ;
#4529=CARTESIAN_POINT ( 'NONE',  ( 0.000000000000000000, 0.000000000000000000, -5.000000000000000888 ) ) ;
#4533=AXIS2_PLACEMENT_3D ( 'NONE', #122, #6746, #1969 ) ;
#4555=ORIENTED_EDGE ( 'NONE', *, *, #3596, .F. ) ;
#4559=CARTESIAN_POINT ( 'NONE',  ( 2.000000000000005329, -3.464101615137751722, 0.000000000000000000 ) ) ;
#4569=AXIS2_PLACEMENT_3D ( 'NONE', #4304, #1697, #4344 ) ;
#4586=CARTESIAN_POINT ( 'NONE',  ( -4.000000000000000888, 1.563622288139195238, -0.2253451193528307472 ) ) ;
#4598=ORIENTED_EDGE ( 'NONE', *, *, #5363, .F. ) ;
#4600=CARTESIAN_POINT ( 'NONE',  ( -4.000000000000000000, 2.309401076758498483, -3.433295621305379353 ) ) ;
#4602=CARTESIAN_POINT ( 'NONE',  ( 4.000000000000000000, 0.8378280264232961239, -3.220590601395640018 ) ) ;
#4625=CARTESIAN_POINT ( 'NONE',  ( 2.059999999999998721, 0.000000000000000000, -0.3080913168122742518 ) ) ;
#4643=CARTESIAN_POINT ( 'NONE',  ( -0.3198814748697807464, -4.434118497892185040, -0.3507732604232532969 ) ) ;
#4644=ORIENTED_EDGE ( 'NONE', *, *, #1300, .F. ) ;
#4646=CARTESIAN_POINT ( 'NONE',  ( -4.000000000000000000, -2.309401076758512694, -3.433295621305382461 ) ) ;
#4649=CARTESIAN_POINT ( 'NONE',  ( 3.999999999999998224, 2.472263674411418588, -3.687027874309861897 ) ) ;
#4650=DIRECTION ( 'NONE',  ( -0.9396926207859138680, 0.000000000000000000, -0.3420201433256536139 ) ) ;
#4662=B_SPLINE_CURVE_WITH_KNOTS ( 'NONE', 3,
 ( #7709, #5038, #5646, #8319, #7234 ),
 .UNSPECIFIED., .F., .F.,
 ( 4, 1, 4 ),
 ( 0.000000000000000000, 0.002309401076758505356, 0.004618802153517010713 ),
 .UNSPECIFIED. ) ;
#4673=VERTEX_POINT ( 'NONE', #6730 ) ;
#4678=CARTESIAN_POINT ( 'NONE',  ( -4.000000000000000000, -2.309401076758512694, -3.433295621305382461 ) ) ;
#4696=LINE ( 'NONE', #3399, #3734 ) ;
#4717=CARTESIAN_POINT ( 'NONE',  ( 4.000000000000000000, -2.309401076758516691, -0.4999999999999995559 ) ) ;
#4721=CYLINDRICAL_SURFACE ( 'NONE', #2009, 2.100000000000000089 ) ;
#4725=ADVANCED_FACE ( 'NONE', ( #5150 ), #441, .T. ) ;
#4728=ORIENTED_EDGE ( 'NONE', *, *, #2524, .F. ) ;
#4729=DIRECTION ( 'NONE',  ( -1.000000000000000000, 0.000000000000000000, 0.000000000000000000 ) ) ;
#4742=ORIENTED_EDGE ( 'NONE', *, *, #1118, .F. ) ;
#4744=DIRECTION ( 'NONE',  ( 1.000000000000000000, 0.000000000000000000, 0.000000000000000000 ) ) ;
#4746=LINE ( 'NONE', #3530, #6847 ) ;
#4750=CARTESIAN_POINT ( 'NONE',  ( 0.000000000000000000, 0.000000000000000000, -5.000000000000000000 ) ) ;
#4751=ORIENTED_EDGE ( 'NONE', *, *, #7174, .T. ) ;
#4754=SHAPE_REPRESENTATION ( 'hex flange nut gradea_iso_ISO - 4161 - M5 - N', ( #594 ), #750 ) ;
#4761=CARTESIAN_POINT ( 'NONE',  ( 5.560781378645573980, 6.809993116116507654E-16, -4.000000000000000000 ) ) ;
#4773=VERTEX_POINT ( 'NONE', #3410 ) ;
#4775=VERTEX_POINT ( 'NONE', #5231 ) ;
#4783=CARTESIAN_POINT ( 'NONE',  ( -3.974344831685191280E-13, 4.796734841935104576, -3.721909803043223608 ) ) ;
#4791=CARTESIAN_POINT ( 'NONE',  ( -3.355112389629170799, 2.681727112203152963, -0.2256878752776689534 ) ) ;
#4798=DIRECTION ( 'NONE',  ( -0.000000000000000000, -0.000000000000000000, 1.000000000000000000 ) ) ;
#4808=ORIENTED_EDGE ( 'NONE', *, *, #5363, .T. ) ;
#4823=CARTESIAN_POINT ( 'NONE',  ( -4.000000000000000000, -2.309401076758512694, -3.433295621305382461 ) ) ;
#4854=CARTESIAN_POINT ( 'NONE',  ( 2.855764796983346177, -2.970025579236428737, -0.09382832055446485575 ) ) ;
#4870=CARTESIAN_POINT ( 'NONE',  ( -4.211140560182196957, -2.431303136016552013, -3.745885042887436178 ) ) ;
#4871=CARTESIAN_POINT ( 'NONE',  ( 3.436319922986518449, -2.634841920959471562, -3.531542292954761741 ) ) ;
#4874=B_SPLINE_CURVE_WITH_KNOTS ( 'NONE', 3,
 ( #2100, #703, #8593, #3450, #7890, #2624 ),
 .UNSPECIFIED., .F., .F.,
 ( 4, 2, 4 ),
 ( -3.640115492410698714E-06, 0.0002066546034006521879, 0.0004169493222937151081 ),
 .UNSPECIFIED. ) ;
#4878=CARTESIAN_POINT ( 'NONE',  ( -3.680118525130244400, 2.494084732383327285, -0.3507732604232449702 ) ) ;
#4880=CARTESIAN_POINT ( 'NONE',  ( 2.500000000000000888, 3.061616997868384127E-16, -4.974599999999998801 ) ) ;
#4890=CARTESIAN_POINT ( 'NONE',  ( 3.999999999999999112, -0.7890432684750902093, -0.04868663549882291247 ) ) ;
#4896=CARTESIAN_POINT ( 'NONE',  ( -4.211140560182196957, -2.431303136016552013, -3.745885042887436178 ) ) ;
#4899=CARTESIAN_POINT ( 'NONE',  ( 0.000000000000000000, 0.000000000000000000, -4.974599999999998801 ) ) ;
#4902=CARTESIAN_POINT ( 'NONE',  ( 0.000000000000000000, 0.000000000000000000, -4.000000000000000000 ) ) ;
#4913=CARTESIAN_POINT ( 'NONE',  ( -0.02448733951239248641, -4.877042772274742255, -3.751161874094027571 ) ) ;
#4920=EDGE_CURVE ( 'NONE', #2573, #7355, #285, .T. ) ;
#4921=CARTESIAN_POINT ( 'NONE',  ( -2.712762565639006418, 3.052587955997511759, -3.430618716626627318 ) ) ;
#4931=CARTESIAN_POINT ( 'NONE',  ( -2.344047193898593395, -3.265465875126480455, -1.054683074273691752E-14 ) ) ;
#4932=CARTESIAN_POINT ( 'NONE',  ( -4.000000000000000000, 2.309401076758498483, -5.000000000000000000 ) ) ;
#4933=CARTESIAN_POINT ( 'NONE',  ( -2.500000000000000444, 3.061616997868383634E-16, -25.03750572909317285 ) ) ;
#4936=EDGE_CURVE ( 'NONE', #7552, #4775, #5305, .T. ) ;
#4938=ORIENTED_EDGE ( 'NONE', *, *, #8555, .F. ) ;
#4951=EDGE_LOOP ( 'NONE', ( #6644, #7444, #1365, #2991, #6672 ) ) ;
#4954=CIRCLE ( 'NONE', #6606, 5.384454397937118664 ) ;
#4968=ORIENTED_EDGE ( 'NONE', *, *, #3025, .T. ) ;
#4971=( LENGTH_UNIT ( ) NAMED_UNIT ( * ) SI_UNIT ( .MILLI., .METRE. ) );
#4979=CARTESIAN_POINT ( 'NONE',  ( -3.472371940586054251, -2.614027278893156669, -3.320322319202162031 ) ) ;
#4984=CARTESIAN_POINT ( 'NONE',  ( 0.000000000000000000, 0.000000000000000000, 0.000000000000000000 ) ) ;
#4988=EDGE_LOOP ( 'NONE', ( #1568, #4644, #813, #5633 ) ) ;
#5005=VECTOR ( 'NONE', #5449, 1000.000000000000000 ) ;
#5015=CARTESIAN_POINT ( 'NONE',  ( 3.349226789952652439, 2.685125164760731487, -0.2236248678334773199 ) ) ;
#5016=CARTESIAN_POINT ( 'NONE',  ( 0.000000000000000000, 0.000000000000000000, -4.484454397937119197 ) ) ;
#5029=CARTESIAN_POINT ( 'NONE',  ( 4.197393957002303999, 7.772902908466098641E-14, -3.503767560748929810 ) ) ;
#5035=( BOUNDED_SURFACE ( )  B_SPLINE_SURFACE ( 3, 2, ( 
 ( #225, #1676, #2337 ),
 ( #4979, #3676, #7596 ),
 ( #4238, #6276, #2380 ),
 ( #8165, #6799, #2198 ),
 ( #181, #2848, #7503 ),
 ( #8298, #5496, #315 ) ),
 .UNSPECIFIED., .F., .F., .F. ) 
 B_SPLINE_SURFACE_WITH_KNOTS ( ( 4, 2, 4 ),
 ( 3, 3 ),
 ( 0.02032853247518126918, 0.02278863295364821906, 0.02524873343211516893 ),
 ( 0.000000000000000000, 1.000000000000000000 ),
 .UNSPECIFIED. ) 
 GEOMETRIC_REPRESENTATION_ITEM ( )  RATIONAL_B_SPLINE_SURFACE ( (
 ( 1.000000000000000000, 0.8047781615896838492, 1.000000000000000000),
 ( 1.000000000000000000, 0.8123767586288186404, 1.000000000000000000),
 ( 1.000000000000000000, 0.8190662415565814758, 1.000000000000000000),
 ( 1.000000000000000000, 0.8192361015667604107, 1.000000000000000000),
 ( 1.000000000000000000, 0.8126135807104967190, 1.000000000000000000),
 ( 1.000000000000000000, 0.8047712338318580017, 1.000000000000000000) ) ) 
 REPRESENTATION_ITEM ( '' )  SURFACE ( )  );
#5038=CARTESIAN_POINT ( 'NONE',  ( -3.333333333333332149, -2.694301256218264218, -3.300726591567082036 ) ) ;
#5041=EDGE_CURVE ( 'NONE', #1514, #771, #6229, .T. ) ;
#5048=DIRECTION ( 'NONE',  ( -0.000000000000000000, -0.000000000000000000, 1.000000000000000000 ) ) ;
#5051=CARTESIAN_POINT ( 'NONE',  ( 0.000000000000000000, 0.000000000000000000, 0.000000000000000000 ) ) ;
#5064=CARTESIAN_POINT ( 'NONE',  ( -6.259644161404860030E-16, -4.618802153517027165, -3.433295621305388234 ) ) ;
#5075=VERTEX_POINT ( 'NONE', #1057 ) ;
#5090=CIRCLE ( 'NONE', #6897, 2.500000000000000444 ) ;
#5106=ORIENTED_EDGE ( 'NONE', *, *, #914, .T. ) ;
#5112=ADVANCED_FACE ( 'NONE', ( #7098 ), #6808, .F. ) ;
#5113=B_SPLINE_CURVE_WITH_KNOTS ( 'NONE', 3,
 ( #774, #2164, #5419, #3428, #7514, #8180, #102, #2208 ),
 .UNSPECIFIED., .F., .F.,
 ( 4, 2, 2, 4 ),
 ( 0.000000000000000000, 0.002450665683189819262, 0.003675998524784728893, 0.004901331366379639391 ),
 .UNSPECIFIED. ) ;
#5121=CARTESIAN_POINT ( 'NONE',  ( -4.204015924366189871, 1.626724848190922446, -3.610627190413390419 ) ) ;
#5144=CARTESIAN_POINT ( 'NONE',  ( -0.6507732100473471171, 4.243078065514775510, -0.2236248678334823436 ) ) ;
#5150=FACE_OUTER_BOUND ( 'NONE', #7460, .T. ) ;
#5158=CARTESIAN_POINT ( 'NONE',  ( 0.6666666666666689611, 4.233901974057261874, -3.300726591567082480 ) ) ;
#5159=CARTESIAN_POINT ( 'NONE',  ( 1.144235203016666258, 3.958177651039090250, -0.09382832055445661235 ) ) ;
#5193=CARTESIAN_POINT ( 'NONE',  ( 4.000000000000000000, -2.309401076758514915, -3.433295621305383349 ) ) ;
#5198=ORIENTED_EDGE ( 'NONE', *, *, #4936, .F. ) ;
#5201=ORIENTED_EDGE ( 'NONE', *, *, #7205, .F. ) ;
#5205=DIRECTION ( 'NONE',  ( 0.000000000000000000, 0.000000000000000000, 1.000000000000000000 ) ) ;
#5207=DIRECTION ( 'NONE',  ( -0.000000000000000000, -0.000000000000000000, 1.000000000000000000 ) ) ;
#5218=AXIS2_PLACEMENT_3D ( 'NONE', #5051, #6354, #4356 ) ;
#5224=CLOSED_SHELL ( 'NONE', ( #1758, #1623, #8236, #2792, #8170, #3844, #6269, #2711, #5328, #1116, #2101, #2933, #8199, #5709, #2061, #2153, #8568, #7109, #1800, #1017, #6156, #8335, #4725, #3350, #2975, #2194, #1122, #5297, #5112, #3906, #748, #2808 ) ) ;
#5231=CARTESIAN_POINT ( 'NONE',  ( 2.000000000000008882, 3.464101615137749945, 0.000000000000000000 ) ) ;
#5233=CARTESIAN_POINT ( 'NONE',  ( 4.000000000000000000, 0.7924765000094659007, -0.05906175389889852662 ) ) ;
#5256=CIRCLE ( 'NONE', #4569, 0.5155456020628804703 ) ;
#5257=DIRECTION ( 'NONE',  ( 0.000000000000000000, 0.000000000000000000, -1.000000000000000000 ) ) ;
#5261=AXIS2_PLACEMENT_3D ( 'NONE', #3, #2676, #4067 ) ;
#5276=ORIENTED_EDGE ( 'NONE', *, *, #4920, .F. ) ;
#5282=EDGE_CURVE ( 'NONE', #3371, #1280, #566, .T. ) ;
#5285=CARTESIAN_POINT ( 'NONE',  ( 2.499999999999999556, 0.000000000000000000, 3.469446951953614189E-15 ) ) ;
#5296=CARTESIAN_POINT ( 'NONE',  ( 4.197478902586992966, -0.8524102783748346290, -3.505063281295504041 ) ) ;
#5297=ADVANCED_FACE ( 'NONE', ( #2014 ), #6200, .F. ) ;
#5300=DIRECTION ( 'NONE',  ( 1.000000000000000000, 0.000000000000000000, 0.000000000000000000 ) ) ;
#5303=ORIENTED_EDGE ( 'NONE', *, *, #5041, .T. ) ;
#5305=CIRCLE ( 'NONE', #6287, 4.000000000000000000 ) ;
#5317=CARTESIAN_POINT ( 'NONE',  ( 3.999999999999999112, 1.941961291383486277, -0.3515519931180248192 ) ) ;
#5319=CARTESIAN_POINT ( 'NONE',  ( 0.000000000000000000, 0.000000000000000000, -5.000000000000000000 ) ) ;
#5325=EDGE_LOOP ( 'NONE', ( #1347, #1453, #1960, #1887, #3603, #7087 ) ) ;
#5328=ADVANCED_FACE ( 'NONE', ( #2917 ), #8195, .T. ) ;
#5336=CARTESIAN_POINT ( 'NONE',  ( 0.000000000000000000, 0.000000000000000000, -4.694516984716113228 ) ) ;
#5339=CARTESIAN_POINT ( 'NONE',  ( -1.144235203016679359, -3.958177651039096911, -0.09382832055446428676 ) ) ;
#5342=EDGE_CURVE ( 'NONE', #6725, #2200, #4746, .T. ) ;
#5346=CARTESIAN_POINT ( 'NONE',  ( 4.204115023516791005, -1.660442669500199919, -3.602151381774560068 ) ) ;
#5350=EDGE_LOOP ( 'NONE', ( #3590, #6683, #4751, #1455 ) ) ;
#5363=EDGE_CURVE ( 'NONE', #1280, #7885, #1443, .T. ) ;
#5390=CARTESIAN_POINT ( 'NONE',  ( 2.807080416178989513, -3.225969019225150003, -3.502507215260505014 ) ) ;
#5394=CARTESIAN_POINT ( 'NONE',  ( -4.000000000000000000, 2.309401076758498483, -5.000000000000000000 ) ) ;
#5411=ORIENTED_EDGE ( 'NONE', *, *, #7205, .T. ) ;
#5412=EDGE_LOOP ( 'NONE', ( #1698, #350, #3287, #2715 ) ) ;
#5419=CARTESIAN_POINT ( 'NONE',  ( 2.805705207896068476, -3.226868319750173075, -3.503898532754370354 ) ) ;
#5426=CARTESIAN_POINT ( 'NONE',  ( -4.024497503033519941, -2.323544716729390558, -3.572167766733381544 ) ) ;
#5427=DIRECTION ( 'NONE',  ( 0.000000000000000000, 0.000000000000000000, -1.000000000000000000 ) ) ;
#5429=CARTESIAN_POINT ( 'NONE',  ( 1.391697335622810172, 4.043246145443375461, -3.503898532754365913 ) ) ;
#5437=PRODUCT_DEFINITION_FORMATION_WITH_SPECIFIED_SOURCE ( 'ANY', '', #1270, .NOT_KNOWN. ) ;
#5447=CARTESIAN_POINT ( 'NONE',  ( -5.384454397937118664, 6.702023979852544604E-16, -5.000000000000000000 ) ) ;
#5449=DIRECTION ( 'NONE',  ( -0.000000000000000000, -0.000000000000000000, 1.000000000000000000 ) ) ;
#5476=CARTESIAN_POINT ( 'NONE',  ( 0.000000000000000000, 0.000000000000000000, -4.974599999999998801 ) ) ;
#5496=CARTESIAN_POINT ( 'NONE',  ( 0.1410422978106145031, -4.700232962125109104, -3.687027686973628704 ) ) ;
#5497=DIRECTION ( 'NONE',  ( 0.000000000000000000, -0.000000000000000000, 1.000000000000000000 ) ) ;
#5513=AXIS2_PLACEMENT_3D ( 'NONE', #5016, #8427, #2980 ) ;
#5515=AXIS2_PLACEMENT_3D ( 'NONE', #6836, #2920, #7492 ) ;
#5517=CARTESIAN_POINT ( 'NONE',  ( -6.473970235329672780E-16, -4.862606272033106691, -3.745885042887442395 ) ) ;
#5524=CARTESIAN_POINT ( 'NONE',  ( -2.725741868435985094, 3.045094352034055429, -3.220599429844047012 ) ) ;
#5526=CARTESIAN_POINT ( 'NONE',  ( -2.059999999999998721, 2.522772406243545965E-16, -0.3080913168122742518 ) ) ;
#5528=LINE ( 'NONE', #4880, #5793 ) ;
#5531=CARTESIAN_POINT ( 'NONE',  ( -4.211140560182196957, 2.431303136016537803, -3.745885042887433514 ) ) ;
#5538=CARTESIAN_POINT ( 'NONE',  ( -6.259644161404860030E-16, -4.618802153517027165, -5.000000000000000000 ) ) ;
#5563=EDGE_LOOP ( 'NONE', ( #2871, #4938, #41, #8264 ) ) ;
#5569=ORIENTED_EDGE ( 'NONE', *, *, #508, .T. ) ;
#5588=ORIENTED_EDGE ( 'NONE', *, *, #4372, .T. ) ;
#5613=DIRECTION ( 'NONE',  ( -0.8191520442889875797, 1.003171929053519570E-16, 0.5735764363510522656 ) ) ;
#5633=ORIENTED_EDGE ( 'NONE', *, *, #3009, .F. ) ;
#5634=CONICAL_SURFACE ( 'NONE', #5218, 4.000000000000000000, 0.8911886515913786111 ) ;
#5643=AXIS2_PLACEMENT_3D ( 'NONE', #988, #4458, #3076 ) ;
#5646=CARTESIAN_POINT ( 'NONE',  ( -2.000000000000002665, -3.464101615137770374, -3.142992957459237680 ) ) ;
#5647=ORIENTED_EDGE ( 'NONE', *, *, #3203, .F. ) ;
#5655=B_SPLINE_CURVE_WITH_KNOTS ( 'NONE', 3,
 ( #4559, #2615, #1434, #652, #110, #7217 ),
 .UNSPECIFIED., .F., .F.,
 ( 4, 2, 4 ),
 ( 0.002365888236227967761, 0.003551327329835077609, 0.004736766423442186590 ),
 .UNSPECIFIED. ) ;
#5662=ORIENTED_EDGE ( 'NONE', *, *, #7637, .T. ) ;
#5664=CARTESIAN_POINT ( 'NONE',  ( -0.1410422978106123659, 4.700232962125094893, -3.687027686973624707 ) ) ;
#5670=CARTESIAN_POINT ( 'NONE',  ( 2.000000000000008882, 3.464101615137749945, 0.000000000000000000 ) ) ;
#5671=CARTESIAN_POINT ( 'NONE',  ( -4.203934362469166963, -1.640673743454851286, -3.598432614606932756 ) ) ;
#5689=CARTESIAN_POINT ( 'NONE',  ( 4.000000000000000000, -2.309401076758514915, -3.433295621305383349 ) ) ;
#5705=DIRECTION ( 'NONE',  ( -1.000000000000000000, 0.000000000000000000, 0.000000000000000000 ) ) ;
#5706=EDGE_CURVE ( 'NONE', #3371, #7420, #7256, .T. ) ;
#5708=DIRECTION ( 'NONE',  ( 1.000000000000000000, 0.000000000000000000, 0.000000000000000000 ) ) ;
#5709=ADVANCED_FACE ( 'NONE', ( #2699, #5859 ), #8535, .F. ) ;
#5721=CARTESIAN_POINT ( 'NONE',  ( -4.000000000000000000, 1.941961291383472732, -0.3515519931180205448 ) ) ;
#5736=EDGE_CURVE ( 'NONE', #1468, #7420, #302, .T. ) ;
#5739=CARTESIAN_POINT ( 'NONE',  ( 0.6666666666666658525, -4.233901974057276085, -3.300726591567086476 ) ) ;
#5764=DIRECTION ( 'NONE',  ( 1.000000000000000000, 0.000000000000000000, 0.000000000000000000 ) ) ;
#5784=CARTESIAN_POINT ( 'NONE',  ( -4.211140560182196957, 2.431303136016537803, -3.745885042887433514 ) ) ;
#5793=VECTOR ( 'NONE', #4228, 1000.000000000000114 ) ;
#5811=CARTESIAN_POINT ( 'NONE',  ( 0.000000000000000000, 0.000000000000000000, 0.000000000000000000 ) ) ;
#5816=VERTEX_POINT ( 'NONE', #7389 ) ;
#5819=CIRCLE ( 'NONE', #7497, 4.000000000000000000 ) ;
#5837=CARTESIAN_POINT ( 'NONE',  ( 4.000000000000000000, 2.309401076758497151, -3.433295621305379353 ) ) ;
#5858=VERTEX_POINT ( 'NONE', #4467 ) ;
#5859=FACE_OUTER_BOUND ( 'NONE', #5325, .T. ) ;
#5884=CARTESIAN_POINT ( 'NONE',  ( 4.000000000000000000, -2.309401076758514915, -5.000000000000000000 ) ) ;
#5890=CARTESIAN_POINT ( 'NONE',  ( -1.317756351988340180, 3.857995168970202116, -0.04852650426601388955 ) ) ;
#5892=ORIENTED_EDGE ( 'NONE', *, *, #8445, .F. ) ;
#5895=CARTESIAN_POINT ( 'NONE',  ( 0.3198814748697593746, 4.434118497892183264, -0.3507732604232499107 ) ) ;
#5902=ORIENTED_EDGE ( 'NONE', *, *, #3010, .T. ) ;
#5903=CARTESIAN_POINT ( 'NONE',  ( -3.999999999999999112, 1.539600717838996324, -3.300726591567078039 ) ) ;
#5924=B_SPLINE_CURVE_WITH_KNOTS ( 'NONE', 3,
 ( #8145, #4215, #2261, #6907, #2867 ),
 .UNSPECIFIED., .F., .F.,
 ( 4, 1, 4 ),
 ( 0.000000000000000000, 0.002309401076758506657, 0.004618802153517013315 ),
 .UNSPECIFIED. ) ;
#5947=CARTESIAN_POINT ( 'NONE',  ( 4.000000000000000888, 0.8228435280416209752, -3.430609588141487976 ) ) ;
#5960=CARTESIAN_POINT ( 'NONE',  ( 2.100000000000000089, 0.000000000000000000, -0.2800830152838844622 ) ) ;
#5962=EDGE_CURVE ( 'NONE', #2893, #926, #8417, .T. ) ;
#5979=VERTEX_POINT ( 'NONE', #2483 ) ;
#6003=ORIENTED_EDGE ( 'NONE', *, *, #1460, .F. ) ;
#6011=DIRECTION ( 'NONE',  ( 0.000000000000000000, 0.000000000000000000, -1.000000000000000000 ) ) ;
#6015=EDGE_LOOP ( 'NONE', ( #5198, #3830, #248 ) ) ;
#6019=EDGE_CURVE ( 'NONE', #917, #1044, #398, .T. ) ;
#6032=ORIENTED_EDGE ( 'NONE', *, *, #8555, .T. ) ;
#6038=EDGE_LOOP ( 'NONE', ( #7601, #5588, #1037, #1098 ) ) ;
#6052=AXIS2_PLACEMENT_3D ( 'NONE', #6161, #6641, #8051 ) ;
#6057=DIRECTION ( 'NONE',  ( -1.000000000000000000, 0.000000000000000000, 0.000000000000000000 ) ) ;
#6059=EDGE_LOOP ( 'NONE', ( #5662, #1822, #5276 ) ) ;
#6074=CARTESIAN_POINT ( 'NONE',  ( 1.567478505476134606E-15, 4.618802153517012066, -3.433295621305382905 ) ) ;
#6078=CARTESIAN_POINT ( 'NONE',  ( 2.449848172108560096, 3.432307619358740514, -3.503702292528905637 ) ) ;
#6080=EDGE_CURVE ( 'NONE', #5816, #7885, #2648, .T. ) ;
#6086=DIRECTION ( 'NONE',  ( -0.8191520442889902442, 0.000000000000000000, -0.5735764363510482688 ) ) ;
#6088=DIRECTION ( 'NONE',  ( 1.000000000000000000, 0.000000000000000000, 0.000000000000000000 ) ) ;
#6091=CARTESIAN_POINT ( 'NONE',  ( -3.679171394226034675, -2.494631558665844739, -0.3503314178412558211 ) ) ;
#6093=AXIS2_PLACEMENT_3D ( 'NONE', #4750, #6617, #6088 ) ;
#6094=CYLINDRICAL_SURFACE ( 'NONE', #6250, 2.100000000000000089 ) ;
#6112=ORIENTED_EDGE ( 'NONE', *, *, #3329, .T. ) ;
#6132=DIRECTION ( 'NONE',  ( 0.000000000000000000, 0.000000000000000000, 1.000000000000000000 ) ) ;
#6138=B_SPLINE_CURVE_WITH_KNOTS ( 'NONE', 3,
 ( #3999, #8487, #2569, #1956 ),
 .UNSPECIFIED., .F., .F.,
 ( 4, 4 ),
 ( 0.000000000000000000, 0.002452478801916361129 ),
 .UNSPECIFIED. ) ;
#6144=CARTESIAN_POINT ( 'NONE',  ( 2.344047193898588954, 3.265465875126468021, -5.031375706690542042E-16 ) ) ;
#6145=FACE_OUTER_BOUND ( 'NONE', #7475, .T. ) ;
#6156=ADVANCED_FACE ( 'NONE', ( #2806 ), #3814, .T. ) ;
#6161=CARTESIAN_POINT ( 'NONE',  ( 0.000000000000000000, 0.000000000000000000, 3.469446951953614189E-15 ) ) ;
#6183=FILL_AREA_STYLE ('',( #262 ) ) ;
#6200=( BOUNDED_SURFACE ( )  B_SPLINE_SURFACE ( 3, 2, ( 
 ( #1350, #4011, #1396 ),
 ( #4050, #2184, #7445 ),
 ( #6222, #4267, #2275 ),
 ( #5524, #4921, #6916 ),
 ( #2876, #6875, #7532 ),
 ( #1613, #7581, #4178 ) ),
 .UNSPECIFIED., .F., .F., .T. ) 
 B_SPLINE_SURFACE_WITH_KNOTS ( ( 4, 2, 4 ),
 ( 3, 3 ),
 ( 0.02032853247518125531, 0.02278863295364820865, 0.02524873343211516200 ),
 ( 0.000000000000000000, 1.000000000000000000 ),
 .UNSPECIFIED. ) 
 GEOMETRIC_REPRESENTATION_ITEM ( )  RATIONAL_B_SPLINE_SURFACE ( (
 ( 1.000000000000000000, 0.8047781615896836271, 1.000000000000000000),
 ( 1.000000000000000000, 0.8123767586289967202, 1.000000000000000000),
 ( 1.000000000000000000, 0.8190662415563443322, 1.000000000000000000),
 ( 1.000000000000000000, 0.8192361015669982205, 1.000000000000000000),
 ( 1.000000000000000000, 0.8126135807103181952, 1.000000000000000000),
 ( 1.000000000000000000, 0.8047712338318587788, 1.000000000000000000) ) ) 
 REPRESENTATION_ITEM ( '' )  SURFACE ( )  );
#6208=ORIENTED_EDGE ( 'NONE', *, *, #1261, .T. ) ;
#6216=CARTESIAN_POINT ( 'NONE',  ( 4.236525694536557474, -2.416953475386482530, -3.751298745799839462 ) ) ;
#6222=CARTESIAN_POINT ( 'NONE',  ( -1.243802165048909503, 3.900692638707381921, -3.223146290109805800 ) ) ;
#6229=LINE ( 'NONE', #264, #6427 ) ;
#6250=AXIS2_PLACEMENT_3D ( 'NONE', #5319, #3983, #6664 ) ;
#6253=CARTESIAN_POINT ( 'NONE',  ( -4.198928548860774157, 0.8158838809860065044, -3.526471437616918170 ) ) ;
#6257=CARTESIAN_POINT ( 'NONE',  ( 2.725741868436127202, -3.045094352033990148, -3.220599429844051453 ) ) ;
#6269=ADVANCED_FACE ( 'NONE', ( #6673 ), #4721, .F. ) ;
#6272=CARTESIAN_POINT ( 'NONE',  ( -4.000000000000000000, -2.309401076758515803, -0.4999999999999995559 ) ) ;
#6274=FACE_OUTER_BOUND ( 'NONE', #2959, .T. ) ;
#6276=CARTESIAN_POINT ( 'NONE',  ( -2.742827927723112236, -3.035229711105190464, -3.433252694550595230 ) ) ;
#6287=AXIS2_PLACEMENT_3D ( 'NONE', #6885, #4798, #6968 ) ;
#6291=ORIENTED_EDGE ( 'NONE', *, *, #442, .T. ) ;
#6301=CARTESIAN_POINT ( 'NONE',  ( 4.101954839143060028, 2.368264730582927857, -3.681130640444267854 ) ) ;
#6310=LINE ( 'NONE', #7090, #3678 ) ;
#6323=CARTESIAN_POINT ( 'NONE',  ( -3.999999999998910649, -1.658469974638591804, -3.531532913075256186 ) ) ;
#6326=CARTESIAN_POINT ( 'NONE',  ( 2.345747346278113987, -3.264484291692503870, -0.01223254789874484924 ) ) ;
#6346=EDGE_LOOP ( 'NONE', ( #8404, #305, #5303, #7310, #8083 ) ) ;
#6352=B_SPLINE_CURVE_WITH_KNOTS ( 'NONE', 3,
 ( #782, #4783, #866, #8275, #3437, #6074 ),
 .UNSPECIFIED., .F., .F.,
 ( 4, 2, 4 ),
 ( -3.640115492407174633E-06, 0.0002066546034006553863, 0.0004169493222937179812 ),
 .UNSPECIFIED. ) ;
#6354=DIRECTION ( 'NONE',  ( 0.000000000000000000, 0.000000000000000000, -1.000000000000000000 ) ) ;
#6360=CARTESIAN_POINT ( 'NONE',  ( 0.5449313310647804220, 4.304185902836899835, -3.316620875263383894 ) ) ;
#6387=DIRECTION ( 'NONE',  ( 1.000000000000000000, 0.000000000000000000, 0.000000000000000000 ) ) ;
#6393=EDGE_LOOP ( 'NONE', ( #1074, #2912, #1483 ) ) ;
#6402=CARTESIAN_POINT ( 'NONE',  ( 2.756197834950227410, 3.027510591568626896, -3.223146290109805356 ) ) ;
#6403=EDGE_CURVE ( 'NONE', #1514, #7097, #6561, .T. ) ;
#6420=ORIENTED_EDGE ( 'NONE', *, *, #400, .F. ) ;
#6422=CARTESIAN_POINT ( 'NONE',  ( -4.000000000000000000, 0.9868501483902560878, -0.09357334158579519445 ) ) ;
#6427=VECTOR ( 'NONE', #2928, 1000.000000000000000 ) ;
#6449=CARTESIAN_POINT ( 'NONE',  ( -0.1756481739660520902, 4.720212674038980261, -3.469390959564065291 ) ) ;
#6455=AXIS2_PLACEMENT_3D ( 'NONE', #8102, #5427, #3480 ) ;
#6460=CARTESIAN_POINT ( 'NONE',  ( 4.000000000000000000, 2.309401076758515803, -0.4999999999999995559 ) ) ;
#6524=DIRECTION ( 'NONE',  ( -1.000000000000000000, 0.000000000000000000, 0.000000000000000000 ) ) ;
#6527=AXIS2_PLACEMENT_3D ( 'NONE', #1319, #709, #2761 ) ;
#6536=CARTESIAN_POINT ( 'NONE',  ( 4.000000000000000888, 1.563622288139206118, -0.2253451193528334950 ) ) ;
#6542=CARTESIAN_POINT ( 'NONE',  ( -1.655952806101422814, 3.662737355149034979, -7.623296525288699970E-18 ) ) ;
#6544=CARTESIAN_POINT ( 'NONE',  ( 2.000000000000000444, 3.464101615137754830, -3.142992957459231018 ) ) ;
#6552=CARTESIAN_POINT ( 'NONE',  ( -1.654252653721913102, -3.663718938583024443, -0.01223254789874440342 ) ) ;
#6561=B_SPLINE_CURVE_WITH_KNOTS ( 'NONE', 3,
 ( #5064, #2986, #3682, #7025, #409, #8430 ),
 .UNSPECIFIED., .F., .F.,
 ( 4, 2, 4 ),
 ( 0.000000000000000000, 0.0002095117440854740156, 0.0004190234881709480313 ),
 .UNSPECIFIED. ) ;
#6562=CARTESIAN_POINT ( 'NONE',  ( 4.000000000000000888, -0.8578082829538523635, -3.433262215449808696 ) ) ;
#6573=CARTESIAN_POINT ( 'NONE',  ( -5.560781378645575757, 6.809993116116508640E-16, -4.000000000000000000 ) ) ;
#6582=CARTESIAN_POINT ( 'NONE',  ( 4.000000000000000000, 0.1981133338132474442, 2.382280164152719704E-17 ) ) ;
#6588=ORIENTED_EDGE ( 'NONE', *, *, #1515, .F. ) ;
#6604=CYLINDRICAL_SURFACE ( 'NONE', #7204, 2.500000000000000444 ) ;
#6605=ORIENTED_EDGE ( 'NONE', *, *, #1515, .T. ) ;
#6606=AXIS2_PLACEMENT_3D ( 'NONE', #8524, #3297, #15 ) ;
#6611=EDGE_CURVE ( 'NONE', #8282, #3127, #2185, .T. ) ;
#6613=CIRCLE ( 'NONE', #6052, 2.499999999999999556 ) ;
#6617=DIRECTION ( 'NONE',  ( -0.000000000000000000, -0.000000000000000000, 1.000000000000000000 ) ) ;
#6641=DIRECTION ( 'NONE',  ( -0.000000000000000000, -0.000000000000000000, 1.000000000000000000 ) ) ;
#6644=ORIENTED_EDGE ( 'NONE', *, *, #3010, .F. ) ;
#6652=EDGE_LOOP ( 'NONE', ( #941, #4524 ) ) ;
#6664=DIRECTION ( 'NONE',  ( 1.000000000000000000, 0.000000000000000000, 0.000000000000000000 ) ) ;
#6672=ORIENTED_EDGE ( 'NONE', *, *, #2022, .F. ) ;
#6673=FACE_OUTER_BOUND ( 'NONE', #3000, .T. ) ;
#6674=CARTESIAN_POINT ( 'NONE',  ( 1.828356344711641102, 3.563200125723180900, -5.433716356636336675E-16 ) ) ;
#6683=ORIENTED_EDGE ( 'NONE', *, *, #2895, .F. ) ;
#6711=FACE_BOUND ( 'NONE', #2652, .T. ) ;
#6725=VERTEX_POINT ( 'NONE', #6960 ) ;
#6730=CARTESIAN_POINT ( 'NONE',  ( -2.500000000000000444, 3.061616997868383634E-16, -5.000000000000000888 ) ) ;
#6737=DIRECTION ( 'NONE',  ( 0.8660254037844374864, -0.5000000000000018874, 0.000000000000000000 ) ) ;
#6746=DIRECTION ( 'NONE',  ( 0.000000000000000000, 0.000000000000000000, -1.000000000000000000 ) ) ;
#6765=( NAMED_UNIT ( * ) SI_UNIT ( $, .STERADIAN. ) SOLID_ANGLE_UNIT ( ) );
#6766=PRODUCT_DEFINITION_SHAPE ( 'NONE', 'NONE',  #7879 ) ;
#6787=CARTESIAN_POINT ( 'NONE',  ( 4.000000000000000000, 2.309401076758497151, -5.000000000000000000 ) ) ;
#6795=EDGE_CURVE ( 'NONE', #1514, #3609, #432, .T. ) ;
#6799=CARTESIAN_POINT ( 'NONE',  ( -1.287237434361707233, -3.875615274277397937, -3.430618716626816500 ) ) ;
#6800=CARTESIAN_POINT ( 'NONE',  ( 0.000000000000000000, 0.000000000000000000, -5.000000000000000888 ) ) ;
#6805=AXIS2_PLACEMENT_3D ( 'NONE', #4529, #4411, #1891 ) ;
#6808=( BOUNDED_SURFACE ( )  B_SPLINE_SURFACE ( 3, 2, ( 
 ( #7725, #3104, #8376 ),
 ( #1187, #2541, #7847 ),
 ( #6402, #3843, #3188 ),
 ( #3669, #1756, #1101 ),
 ( #6360, #3711, #2502 ),
 ( #6449, #5664, #396 ) ),
 .UNSPECIFIED., .F., .F., .T. ) 
 B_SPLINE_SURFACE_WITH_KNOTS ( ( 4, 2, 4 ),
 ( 3, 3 ),
 ( 0.02032853247518126225, 0.02278863295364821212, 0.02524873343211516200 ),
 ( 0.000000000000000000, 1.000000000000000000 ),
 .UNSPECIFIED. ) 
 GEOMETRIC_REPRESENTATION_ITEM ( )  RATIONAL_B_SPLINE_SURFACE ( (
 ( 1.000000000000000000, 0.8047781615896835161, 1.000000000000000000),
 ( 1.000000000000000000, 0.8123767586291043008, 1.000000000000000000),
 ( 1.000000000000000000, 0.8190662415562011134, 1.000000000000000000),
 ( 1.000000000000000000, 0.8192361015671398849, 1.000000000000000000),
 ( 1.000000000000000000, 0.8126135807102121689, 1.000000000000000000),
 ( 1.000000000000000000, 0.8047712338318585568, 1.000000000000000000) ) ) 
 REPRESENTATION_ITEM ( '' )  SURFACE ( )  );
#6820=B_SPLINE_CURVE_WITH_KNOTS ( 'NONE', 3,
 ( #3176, #4643, #2572, #5339, #7300, #6552, #688, #3302 ),
 .UNSPECIFIED., .F., .F.,
 ( 4, 2, 2, 4 ),
 ( 2.465131517390770070E-07, 0.001183067374689869946, 0.001774477805458935659, 0.002365888236228001588 ),
 .UNSPECIFIED. ) ;
#6826=CARTESIAN_POINT ( 'NONE',  ( -4.211140560182196957, -2.431303136016552013, -3.745885042887436178 ) ) ;
#6836=CARTESIAN_POINT ( 'NONE',  ( 0.000000000000000000, 0.000000000000000000, -4.000000000000000000 ) ) ;
#6840=SURFACE_STYLE_USAGE ( .BOTH. , #3667 ) ;
#6847=VECTOR ( 'NONE', #4224, 1000.000000000000000 ) ;
#6848=CARTESIAN_POINT ( 'NONE',  ( 4.000000000000000000, 2.309401076758515803, -0.4999999999999995559 ) ) ;
#6849=PLANE ( 'NONE',  #2872 ) ;
#6850=EDGE_CURVE ( 'NONE', #4209, #5979, #6310, .T. ) ;
#6853=CARTESIAN_POINT ( 'NONE',  ( 2.171643655288379993, -3.365003104552334978, -1.195831703456429434E-14 ) ) ;
#6857=VERTEX_POINT ( 'NONE', #3789 ) ;
#6870=FACE_OUTER_BOUND ( 'NONE', #6346, .T. ) ;
#6875=CARTESIAN_POINT ( 'NONE',  ( -3.436319922987618902, 2.634841920961291439, -3.531542292955721862 ) ) ;
#6885=CARTESIAN_POINT ( 'NONE',  ( 0.000000000000000000, 0.000000000000000000, 0.000000000000000000 ) ) ;
#6890=CARTESIAN_POINT ( 'NONE',  ( -4.000000000000000000, 2.309401076758498483, -3.433295621305379353 ) ) ;
#6897=AXIS2_PLACEMENT_3D ( 'NONE', #6800, #5497, #8126 ) ;
#6902=ORIENTED_EDGE ( 'NONE', *, *, #2895, .T. ) ;
#6906=CIRCLE ( 'NONE', #2459, 2.500000000000000888 ) ;
#6907=CARTESIAN_POINT ( 'NONE',  ( -3.333333333333335258, 2.694301256218251783, -3.300726591567079815 ) ) ;
#6911=CARTESIAN_POINT ( 'NONE',  ( -2.449848172108560540, -3.432307619358754724, -3.503702292528910078 ) ) ;
#6912=CARTESIAN_POINT ( 'NONE',  ( 0.6640947660595348800, -4.471078309994175548, -3.602146406945708090 ) ) ;
#6916=CARTESIAN_POINT ( 'NONE',  ( -2.807080416178626692, 3.225969019225154444, -3.502507215260441065 ) ) ;
#6922=EDGE_LOOP ( 'NONE', ( #947, #6588 ) ) ;
#6930=CARTESIAN_POINT ( 'NONE',  ( -4.197312064133472020, -0.8182229787990021874, -3.502518405183886685 ) ) ;
#6934=ORIENTED_EDGE ( 'NONE', *, *, #1300, .T. ) ;
#6960=CARTESIAN_POINT ( 'NONE',  ( 2.100000000000000089, 0.000000000000000000, -4.694516984716113228 ) ) ;
#6966=( NAMED_UNIT ( * ) SI_UNIT ( $, .STERADIAN. ) SOLID_ANGLE_UNIT ( ) );
#6968=DIRECTION ( 'NONE',  ( 1.000000000000000000, 0.000000000000000000, 0.000000000000000000 ) ) ;
#6969=CARTESIAN_POINT ( 'NONE',  ( 5.560781378645575757, 0.000000000000000000, -4.000000000000000000 ) ) ;
#6994=MECHANICAL_DESIGN_GEOMETRIC_PRESENTATION_REPRESENTATION('',(#33),#7706);
#7008=EDGE_CURVE ( 'NONE', #7420, #7355, #2051, .T. ) ;
#7022=CARTESIAN_POINT ( 'NONE',  ( -4.000000000000000000, -1.680117682357936904, -3.316611593218794951 ) ) ;
#7025=CARTESIAN_POINT ( 'NONE',  ( -1.240299975428134203E-15, -4.736529461165891242, -3.681130640444276292 ) ) ;
#7039=AXIS2_PLACEMENT_3D ( 'NONE', #8477, #8396, #2438 ) ;
#7042=LINE ( 'NONE', #5884, #682 ) ;
#7062=FACE_OUTER_BOUND ( 'NONE', #658, .T. ) ;
#7074=VERTEX_POINT ( 'NONE', #4091 ) ;
#7083=CIRCLE ( 'NONE', #3337, 5.560781378645573980 ) ;
#7087=ORIENTED_EDGE ( 'NONE', *, *, #175, .F. ) ;
#7090=CARTESIAN_POINT ( 'NONE',  ( 2.500000000000000444, 0.000000000000000000, -25.03750572909317285 ) ) ;
#7094=( BOUNDED_SURFACE ( )  B_SPLINE_SURFACE ( 3, 2, ( 
 ( #8188, #1474, #4913 ),
 ( #4171, #154, #6912 ),
 ( #7526, #3483, #3440 ),
 ( #6257, #2870, #5390 ),
 ( #2220, #4871, #1564 ),
 ( #913, #3567, #6216 ) ),
 .UNSPECIFIED., .F., .F., .F. ) 
 B_SPLINE_SURFACE_WITH_KNOTS ( ( 4, 2, 4 ),
 ( 3, 3 ),
 ( 0.02032853247518126918, 0.02278863295364821906, 0.02524873343211517240 ),
 ( 0.000000000000000000, 1.000000000000000000 ),
 .UNSPECIFIED. ) 
 GEOMETRIC_REPRESENTATION_ITEM ( )  RATIONAL_B_SPLINE_SURFACE ( (
 ( 1.000000000000000000, 0.8047781615896837382, 1.000000000000000000),
 ( 1.000000000000000000, 0.8123767586289252218, 1.000000000000000000),
 ( 1.000000000000000000, 0.8190662415564388121, 1.000000000000000000),
 ( 1.000000000000000000, 0.8192361015669026303, 1.000000000000000000),
 ( 1.000000000000000000, 0.8126135807103900266, 1.000000000000000000),
 ( 1.000000000000000000, 0.8047712338318593339, 1.000000000000000000) ) ) 
 REPRESENTATION_ITEM ( '' )  SURFACE ( )  );
#7097=VERTEX_POINT ( 'NONE', #2217 ) ;
#7098=FACE_OUTER_BOUND ( 'NONE', #5350, .T. ) ;
#7100=B_SPLINE_CURVE_WITH_KNOTS ( 'NONE', 3,
 ( #5517, #2218, #4259, #6911, #956, #3607, #4131, #4870 ),
 .UNSPECIFIED., .F., .F.,
 ( 4, 2, 2, 4 ),
 ( 0.000000000000000000, 0.002450665683189818828, 0.003675998524784728459, 0.004901331366379638524 ),
 .UNSPECIFIED. ) ;
#7109=ADVANCED_FACE ( 'NONE', ( #1561 ), #1595, .T. ) ;
#7124=DIRECTION ( 'NONE',  ( -0.000000000000000000, -0.000000000000000000, 1.000000000000000000 ) ) ;
#7134=ORIENTED_EDGE ( 'NONE', *, *, #3203, .T. ) ;
#7164=CARTESIAN_POINT ( 'NONE',  ( 2.000000000000008882, 3.464101615137749945, 0.000000000000000000 ) ) ;
#7174=EDGE_CURVE ( 'NONE', #1258, #1044, #6352, .T. ) ;
#7204=AXIS2_PLACEMENT_3D ( 'NONE', #2402, #2705, #5300 ) ;
#7205=EDGE_CURVE ( 'NONE', #1044, #3371, #5924, .T. ) ;
#7217=CARTESIAN_POINT ( 'NONE',  ( -2.688821387764050996E-14, -4.618802153517012954, -0.4999999999999995559 ) ) ;
#7234=CARTESIAN_POINT ( 'NONE',  ( -6.259644161404860030E-16, -4.618802153517027165, -3.433295621305388234 ) ) ;
#7249=ORIENTED_EDGE ( 'NONE', *, *, #8202, .T. ) ;
#7256=B_SPLINE_CURVE_WITH_KNOTS ( 'NONE', 3,
 ( #4600, #5903, #3220, #7258, #4646 ),
 .UNSPECIFIED., .F., .F.,
 ( 4, 1, 4 ),
 ( 0.000000000000000000, 0.002309401076758505790, 0.004618802153517011580 ),
 .UNSPECIFIED. ) ;
#7258=CARTESIAN_POINT ( 'NONE',  ( -4.000000000000000888, -1.539600717839011201, -3.300726591567081591 ) ) ;
#7271=EDGE_CURVE ( 'NONE', #7074, #5979, #7977, .T. ) ;
#7282=CARTESIAN_POINT ( 'NONE',  ( 4.101954839143059139, -2.368264730582948285, -3.681130640444269631 ) ) ;
#7285=DIRECTION ( 'NONE',  ( 0.8191520442889875797, 0.000000000000000000, 0.5735764363510522656 ) ) ;
#7297=DIRECTION ( 'NONE',  ( -0.000000000000000000, -0.000000000000000000, 1.000000000000000000 ) ) ;
#7300=CARTESIAN_POINT ( 'NONE',  ( -1.312671235360383548, -3.860931062424228788, -0.05923475698271369466 ) ) ;
#7308=CARTESIAN_POINT ( 'NONE',  ( 4.211405965630455661, 2.460463115436283932, -3.751298928144577882 ) ) ;
#7310=ORIENTED_EDGE ( 'NONE', *, *, #4499, .T. ) ;
#7355=VERTEX_POINT ( 'NONE', #8446 ) ;
#7385=SHAPE_DEFINITION_REPRESENTATION ( #6766, #4754 ) ;
#7389=CARTESIAN_POINT ( 'NONE',  ( -4.000000000000000000, 0.000000000000000000, 0.000000000000000000 ) ) ;
#7398=ORIENTED_EDGE ( 'NONE', *, *, #442, .F. ) ;
#7400=CARTESIAN_POINT ( 'NONE',  ( -2.687328764639638656, 3.067272167851286202, -0.05923475698270370959 ) ) ;
#7420=VERTEX_POINT ( 'NONE', #4678 ) ;
#7429=DIRECTION ( 'NONE',  ( -0.000000000000000000, 0.000000000000000000, -1.000000000000000000 ) ) ;
#7437=CARTESIAN_POINT ( 'NONE',  ( 1.411581201560190495E-15, 4.862606272033091592, -3.745885042887436622 ) ) ;
#7444=ORIENTED_EDGE ( 'NONE', *, *, #1401, .T. ) ;
#7445=CARTESIAN_POINT ( 'NONE',  ( -0.6640947660597427138, 4.471078309994878985, -3.602146406945963442 ) ) ;
#7455=VECTOR ( 'NONE', #1452, 1000.000000000000227 ) ;
#7460=EDGE_LOOP ( 'NONE', ( #7398, #3484, #4598 ) ) ;
#7461=ORIENTED_EDGE ( 'NONE', *, *, #6019, .T. ) ;
#7462=DIRECTION ( 'NONE',  ( -1.000000000000000000, 0.000000000000000000, 0.000000000000000000 ) ) ;
#7475=EDGE_LOOP ( 'NONE', ( #8084, #3449, #5902, #3599, #96 ) ) ;
#7492=DIRECTION ( 'NONE',  ( 1.000000000000000000, 0.000000000000000000, 0.000000000000000000 ) ) ;
#7495=CARTESIAN_POINT ( 'NONE',  ( 0.000000000000000000, 0.000000000000000000, 0.000000000000000000 ) ) ;
#7497=AXIS2_PLACEMENT_3D ( 'NONE', #7495, #927, #307 ) ;
#7503=CARTESIAN_POINT ( 'NONE',  ( -0.6810597143197697489, -4.461075778259609770, -3.598441714920717516 ) ) ;
#7514=CARTESIAN_POINT ( 'NONE',  ( 1.393927851585479161, -4.043713361053543842, -3.526374918436840922 ) ) ;
#7519=EDGE_CURVE ( 'NONE', #3408, #4775, #3141, .T. ) ;
#7526=CARTESIAN_POINT ( 'NONE',  ( 1.243802165048773611, -3.900692638707475624, -3.223146290109810241 ) ) ;
#7531=ORIENTED_EDGE ( 'NONE', *, *, #7818, .T. ) ;
#7532=CARTESIAN_POINT ( 'NONE',  ( -3.522875095019672109, 2.820352903225427532, -3.598441714920591394 ) ) ;
#7552=VERTEX_POINT ( 'NONE', #7827 ) ;
#7560=STYLED_ITEM ( 'NONE', ( #218 ), #759 ) ;
#7573=MANIFOLD_SOLID_BREP ( 'EndChamfer', #5224 ) ;
#7576=DIRECTION ( 'NONE',  ( -0.5000000000000019984, -0.8660254037844375974, 0.000000000000000000 ) ) ;
#7581=CARTESIAN_POINT ( 'NONE',  ( -4.141042297810615835, 2.227970268150415656, -3.687027686973619822 ) ) ;
#7587=CARTESIAN_POINT ( 'NONE',  ( -3.511755186886750479, 2.826662030176366081, -3.597382984111578086 ) ) ;
#7588=( NAMED_UNIT ( * ) SI_UNIT ( $, .STERADIAN. ) SOLID_ANGLE_UNIT ( ) );
#7596=CARTESIAN_POINT ( 'NONE',  ( -3.540020015735593439, -2.810662092924100630, -3.602146406945814672 ) ) ;
#7597=ORIENTED_EDGE ( 'NONE', *, *, #3865, .F. ) ;
#7598=CIRCLE ( 'NONE', #4257, 0.5155456020628804703 ) ;
#7601=ORIENTED_EDGE ( 'NONE', *, *, #6611, .F. ) ;
#7637=EDGE_CURVE ( 'NONE', #2573, #5816, #4087, .T. ) ;
#7641=CARTESIAN_POINT ( 'NONE',  ( -4.000000000000000000, 0.8730739991738342143, -3.223134629628428893 ) ) ;
#7661=CARTESIAN_POINT ( 'NONE',  ( 4.204015924366189871, -1.626724848190933548, -3.610627190413393084 ) ) ;
#7682=FACE_OUTER_BOUND ( 'NONE', #2772, .T. ) ;
#7685=CARTESIAN_POINT ( 'NONE',  ( 2.682243648011666703, 3.070208061305304881, -0.04852650426601266831 ) ) ;
#7693=UNCERTAINTY_MEASURE_WITH_UNIT (LENGTH_MEASURE( 1.000000000000000082E-05 ), #2030, 'distance_accuracy_value', 'NONE');
#7706=( GEOMETRIC_REPRESENTATION_CONTEXT ( 3 ) GLOBAL_UNCERTAINTY_ASSIGNED_CONTEXT ( ( #4071 ) ) GLOBAL_UNIT_ASSIGNED_CONTEXT ( ( #2770, #137, #6765 ) ) REPRESENTATION_CONTEXT ( 'NONE', 'WORKASPACE' ) );
#7709=CARTESIAN_POINT ( 'NONE',  ( -4.000000000000000000, -2.309401076758512694, -3.433295621305382461 ) ) ;
#7719=CARTESIAN_POINT ( 'NONE',  ( 4.000000000000000000, -2.309401076758516691, -0.4999999999999995559 ) ) ;
#7725=CARTESIAN_POINT ( 'NONE',  ( 4.175002511812151873, 2.208363329454889445, -3.469254087858244073 ) ) ;
#7732=ORIENTED_EDGE ( 'NONE', *, *, #914, .F. ) ;
#7760=FACE_OUTER_BOUND ( 'NONE', #2819, .T. ) ;
#7770=CARTESIAN_POINT ( 'NONE',  ( -4.000000000000000000, 2.471528634177585282, -3.686887442155186712 ) ) ;
#7773=DIRECTION ( 'NONE',  ( -1.000000000000000000, 0.000000000000000000, 0.000000000000000000 ) ) ;
#7783=ORIENTED_EDGE ( 'NONE', *, *, #1261, .F. ) ;
#7787=CARTESIAN_POINT ( 'NONE',  ( 4.197393957002303999, 7.772902908466098641E-14, -3.503767560748929810 ) ) ;
#7818=EDGE_CURVE ( 'NONE', #3609, #596, #4159, .T. ) ;
#7821=AXIS2_PLACEMENT_3D ( 'NONE', #1584, #3714, #311 ) ;
#7827=CARTESIAN_POINT ( 'NONE',  ( 4.000000000000000000, 0.000000000000000000, 0.000000000000000000 ) ) ;
#7847=CARTESIAN_POINT ( 'NONE',  ( 3.540020015735602765, 2.810662092924382627, -3.602146406945867962 ) ) ;
#7858=CARTESIAN_POINT ( 'NONE',  ( 3.999999999999999112, 2.309401076758497595, -3.504271511726784194 ) ) ;
#7861=LINE ( 'NONE', #1865, #8437 ) ;
#7865=EDGE_CURVE ( 'NONE', #7552, #5858, #3334, .T. ) ;
#7879=PRODUCT_DEFINITION ( 'UNKNOWN', '', #5437, #3254 ) ;
#7880=PLANE ( 'NONE',  #8013 ) ;
#7885=VERTEX_POINT ( 'NONE', #670 ) ;
#7890=CARTESIAN_POINT ( 'NONE',  ( -4.000000000000004441, 2.309401076758496263, -3.504269196027523847 ) ) ;
#7893=B_SPLINE_CURVE_WITH_KNOTS ( 'NONE', 3,
 ( #7437, #3525, #5429, #6078, #1608, #1435, #869, #2911 ),
 .UNSPECIFIED., .F., .F.,
 ( 4, 2, 2, 4 ),
 ( 7.780516681398759253E-20, 0.002450665683189819696, 0.003675998524784729327, 0.004901331366379639391 ),
 .UNSPECIFIED. ) ;
#7914=AXIS2_PLACEMENT_3D ( 'NONE', #4094, #7576, #6737 ) ;
#7923=DIRECTION ( 'NONE',  ( -1.000000000000000000, 0.000000000000000000, 0.000000000000000000 ) ) ;
#7930=AXIS2_PLACEMENT_3D ( 'NONE', #91, #6011, #4024 ) ;
#7933=FACE_OUTER_BOUND ( 'NONE', #2352, .T. ) ;
#7948=ORIENTED_EDGE ( 'NONE', *, *, #5736, .T. ) ;
#7956=VERTEX_POINT ( 'NONE', #5447 ) ;
#7970=CARTESIAN_POINT ( 'NONE',  ( 4.000000000001088907, 1.658577278524410170, -3.531553309554541720 ) ) ;
#7977=CIRCLE ( 'NONE', #4220, 2.500000000000000888 ) ;
#7978=COLOUR_RGB ( '',1.000000000000000000, 0.9490196078431372140, 0.9098039215686274384 ) ;
#7990=FACE_OUTER_BOUND ( 'NONE', #192, .T. ) ;
#8013=AXIS2_PLACEMENT_3D ( 'NONE', #4007, #7923, #1343 ) ;
#8022=B_SPLINE_CURVE_WITH_KNOTS ( 'NONE', 3,
 ( #2243, #3071, #3681, #4854, #2385, #6326, #6853, #364 ),
 .UNSPECIFIED., .F., .F.,
 ( 4, 2, 2, 4 ),
 ( 2.465131517071610173E-07, 0.001183067374689837636, 0.001774477805458902699, 0.002365888236227967761 ),
 .UNSPECIFIED. ) ;
#8025=AXIS2_PLACEMENT_3D ( 'NONE', #5538, #131, #2801 ) ;
#8039=CARTESIAN_POINT ( 'NONE',  ( 4.000000000000000000, 0.000000000000000000, 0.000000000000000000 ) ) ;
#8051=DIRECTION ( 'NONE',  ( 1.000000000000000000, 0.000000000000000000, 0.000000000000000000 ) ) ;
#8060=CARTESIAN_POINT ( 'NONE',  ( 4.203935335434060505, 1.640780671294165272, -3.598452447879202598 ) ) ;
#8067=ORIENTED_EDGE ( 'NONE', *, *, #8202, .F. ) ;
#8077=CIRCLE ( 'NONE', #7930, 2.100000000000000089 ) ;
#8083=ORIENTED_EDGE ( 'NONE', *, *, #4920, .T. ) ;
#8084=ORIENTED_EDGE ( 'NONE', *, *, #5041, .F. ) ;
#8095=APPLICATION_CONTEXT ( 'automotive_design' ) ;
#8101=CARTESIAN_POINT ( 'NONE',  ( -4.000000000000000888, -2.309401076758512694, -3.504269196027526512 ) ) ;
#8102=CARTESIAN_POINT ( 'NONE',  ( 0.000000000000000000, 0.000000000000000000, 0.000000000000000000 ) ) ;
#8105=PLANE ( 'NONE',  #7914 ) ;
#8113=AXIS2_PLACEMENT_3D ( 'NONE', #4932, #5705, #2422 ) ;
#8123=LINE ( 'NONE', #4933, #5005 ) ;
#8126=DIRECTION ( 'NONE',  ( -1.000000000000000000, 0.000000000000000000, 0.000000000000000000 ) ) ;
#8130=ORIENTED_EDGE ( 'NONE', *, *, #400, .T. ) ;
#8131=VERTEX_POINT ( 'NONE', #6969 ) ;
#8132=DIRECTION ( 'NONE',  ( 0.000000000000000000, 0.000000000000000000, -1.000000000000000000 ) ) ;
#8135=ORIENTED_EDGE ( 'NONE', *, *, #1315, .T. ) ;
#8145=CARTESIAN_POINT ( 'NONE',  ( 1.567478505476134606E-15, 4.618802153517012066, -3.433295621305382905 ) ) ;
#8150=CARTESIAN_POINT ( 'NONE',  ( -4.197393957002303999, -7.773935952363655451E-14, -3.503767560748929810 ) ) ;
#8165=CARTESIAN_POINT ( 'NONE',  ( -1.274258131565027874, -3.883108878240886241, -3.220599429844051009 ) ) ;
#8166=LINE ( 'NONE', #4761, #7455 ) ;
#8170=ADVANCED_FACE ( 'NONE', ( #6274 ), #1012, .T. ) ;
#8180=CARTESIAN_POINT ( 'NONE',  ( 0.6937372685066666156, -4.453844082567737672, -3.610536846335894445 ) ) ;
#8187=CARTESIAN_POINT ( 'NONE',  ( -4.000000000000000000, 2.309401076758498483, -0.4999999999999927280 ) ) ;
#8188=CARTESIAN_POINT ( 'NONE',  ( -0.1750025118121544265, -4.719839900820635314, -3.469254087858253399 ) ) ;
#8192=CARTESIAN_POINT ( 'NONE',  ( -4.197393957002303999, -0.8151795401431414234, -3.503767560748935139 ) ) ;
#8195=PLANE ( 'NONE',  #1433 ) ;
#8199=ADVANCED_FACE ( 'NONE', ( #7682 ), #3065, .T. ) ;
#8202=EDGE_CURVE ( 'NONE', #1468, #2893, #3955, .T. ) ;
#8203=CARTESIAN_POINT ( 'NONE',  ( -0.6937372685066653943, 4.453844082567723461, -3.610536846335889116 ) ) ;
#8219=ORIENTED_EDGE ( 'NONE', *, *, #3025, .F. ) ;
#8220=DIRECTION ( 'NONE',  ( 0.000000000000000000, 0.000000000000000000, -1.000000000000000000 ) ) ;
#8231=DIRECTION ( 'NONE',  ( 1.000000000000000000, 0.000000000000000000, 0.000000000000000000 ) ) ;
#8236=ADVANCED_FACE ( 'NONE', ( #2092 ), #1569, .F. ) ;
#8264=ORIENTED_EDGE ( 'NONE', *, *, #6795, .F. ) ;
#8265=DIRECTION ( 'NONE',  ( 1.224646799147353207E-16, 1.000000000000000000, 0.000000000000000000 ) ) ;
#8272=ORIENTED_EDGE ( 'NONE', *, *, #1652, .F. ) ;
#8275=CARTESIAN_POINT ( 'NONE',  ( 2.290893957444128645E-15, 4.647089433458768681, -3.572167766733382877 ) ) ;
#8282=VERTEX_POINT ( 'NONE', #2833 ) ;
#8284=CARTESIAN_POINT ( 'NONE',  ( -4.000000000000000000, 2.309401076758498483, -0.4999999999999927280 ) ) ;
#8289=CARTESIAN_POINT ( 'NONE',  ( -2.500000000000000888, 0.000000000000000000, -4.974599999999998801 ) ) ;
#8294=CARTESIAN_POINT ( 'NONE',  ( -2.000000000000007550, -3.464101615137749945, 0.000000000000000000 ) ) ;
#8298=CARTESIAN_POINT ( 'NONE',  ( 0.1756481739660539498, -4.720212674038995360, -3.469390959564070620 ) ) ;
#8300=ORIENTED_EDGE ( 'NONE', *, *, #1351, .F. ) ;
#8318=CARTESIAN_POINT ( 'NONE',  ( -4.000000000000000000, -0.3979232138631226823, -3.896351557369779711E-17 ) ) ;
#8319=CARTESIAN_POINT ( 'NONE',  ( -0.6666666666666666297, -4.233901974057276973, -3.300726591567087365 ) ) ;
#8323=ORIENTED_EDGE ( 'NONE', *, *, #7519, .T. ) ;
#8335=ADVANCED_FACE ( 'NONE', ( #831 ), #881, .T. ) ;
#8340=CARTESIAN_POINT ( 'NONE',  ( -4.000000000000000000, -2.512220745329312610, -3.469390707569719901 ) ) ;
#8352=VECTOR ( 'NONE', #7285, 999.9999999999998863 ) ;
#8359=EDGE_CURVE ( 'NONE', #1490, #3127, #3373, .T. ) ;
#8362=ORIENTED_EDGE ( 'NONE', *, *, #5282, .F. ) ;
#8364=DIRECTION ( 'NONE',  ( 1.000000000000000000, 0.000000000000000000, 0.000000000000000000 ) ) ;
#8376=CARTESIAN_POINT ( 'NONE',  ( 4.235886605889389145, 2.417314728048528760, -3.751161874094018245 ) ) ;
#8394=EDGE_CURVE ( 'NONE', #4773, #6725, #1991, .T. ) ;
#8396=DIRECTION ( 'NONE',  ( 0.000000000000000000, 0.000000000000000000, -1.000000000000000000 ) ) ;
#8404=ORIENTED_EDGE ( 'NONE', *, *, #7008, .F. ) ;
#8413=ORIENTED_EDGE ( 'NONE', *, *, #5706, .T. ) ;
#8415=CARTESIAN_POINT ( 'NONE',  ( 3.333333333333335702, -2.694301256218268215, -3.300726591567084256 ) ) ;
#8417=B_SPLINE_CURVE_WITH_KNOTS ( 'NONE', 3,
 ( #1039, #4426, #6253, #5121, #1650, #4299 ),
 .UNSPECIFIED., .F., .F.,
 ( 4, 2, 4 ),
 ( 0.002452478801916376308, 0.003676905084148007850, 0.004901331366379639391 ),
 .UNSPECIFIED. ) ;
#8424=CARTESIAN_POINT ( 'NONE',  ( 1.734723475976807094E-15, 4.618802153517012954, -0.4999999999999995559 ) ) ;
#8427=DIRECTION ( 'NONE',  ( -0.000000000000000000, -0.000000000000000000, 1.000000000000000000 ) ) ;
#8430=CARTESIAN_POINT ( 'NONE',  ( -6.473970235329672780E-16, -4.862606272033106691, -3.745885042887442395 ) ) ;
#8437=VECTOR ( 'NONE', #1119, 1000.000000000000000 ) ;
#8445=EDGE_CURVE ( 'NONE', #5075, #392, #6138, .T. ) ;
#8446=CARTESIAN_POINT ( 'NONE',  ( -4.000000000000000000, -2.309401076758515803, -0.4999999999999995559 ) ) ;
#8449=CARTESIAN_POINT ( 'NONE',  ( -4.000000000000000000, 0.000000000000000000, 0.000000000000000000 ) ) ;
#8465=EDGE_CURVE ( 'NONE', #1114, #2573, #1432, .T. ) ;
#8472=VECTOR ( 'NONE', #6132, 1000.000000000000000 ) ;
#8477=CARTESIAN_POINT ( 'NONE',  ( 0.000000000000000000, 0.000000000000000000, 0.000000000000000000 ) ) ;
#8482=CIRCLE ( 'NONE', #6093, 5.384454397937118664 ) ;
#8487=CARTESIAN_POINT ( 'NONE',  ( 4.203833317240879275, 1.627343821129582979, -3.597273115243889929 ) ) ;
#8509=CARTESIAN_POINT ( 'NONE',  ( 4.024499207728657879, -2.323545700935587988, -3.572172305156509964 ) ) ;
#8512=CARTESIAN_POINT ( 'NONE',  ( 4.024499207728657879, 2.323545700935571556, -3.572172305156506411 ) ) ;
#8524=CARTESIAN_POINT ( 'NONE',  ( 0.000000000000000000, 0.000000000000000000, -5.000000000000000000 ) ) ;
#8535=PLANE ( 'NONE',  #1871 ) ;
#8555=EDGE_CURVE ( 'NONE', #596, #7097, #5113, .T. ) ;
#8562=ORIENTED_EDGE ( 'NONE', *, *, #8394, .T. ) ;
#8564=CARTESIAN_POINT ( 'NONE',  ( 1.312671235360372224, 3.860931062424219462, -0.05923475698270440348 ) ) ;
#8568=ADVANCED_FACE ( 'NONE', ( #2775 ), #2962, .T. ) ;
#8593=CARTESIAN_POINT ( 'NONE',  ( -4.101948962585906244, 2.368261337751074169, -3.681124513963621503 ) ) ;
#8665=COLOUR_RGB('Black',0.12,0.14,0.17);
#8666=FILL_AREA_STYLE_COLOUR('',#8665);
#8667=FILL_AREA_STYLE('',(#8666));
#8668=SURFACE_STYLE_FILL_AREA(#8667);
#8669=SURFACE_SIDE_STYLE('',(#8668));
#8670=SURFACE_STYLE_USAGE(.BOTH.,#8669);
#8671=PRESENTATION_STYLE_ASSIGNMENT((#8670));
ENDSEC;
END-ISO-10303-21;
